ISO-10303-21;
HEADER;
/* Generated by software containing ST-Developer
 * from STEP Tools, Inc. (www.steptools.com) 
 */

FILE_DESCRIPTION(
/* description */ (''),
/* implementation_level */ '2;1');

FILE_NAME(
/* name */ 'CarregeSupport(Mirror).step',
/* time_stamp */ '2026-10-05T11:01:41-07:00',
/* author */ (''),
/* organization */ (''),
/* preprocessor_version */ 'ST-DEVELOPER v20.2',
/* originating_system */ 'Autodesk Translation Framework v15.15.0.0',
/* authorisation */ '');

FILE_SCHEMA (('AUTOMOTIVE_DESIGN { 1 0 10303 214 3 1 1 }'));
ENDSEC;

DATA;
#10=MECHANICAL_DESIGN_GEOMETRIC_PRESENTATION_REPRESENTATION('',(#2141),#215609);
#51=SPHERICAL_SURFACE('',#29024,0.5);
#52=SPHERICAL_SURFACE('',#29026,0.5);
#53=SPHERICAL_SURFACE('',#29065,0.5);
#54=SPHERICAL_SURFACE('',#29071,0.5);
#59=(
BOUNDED_SURFACE()
B_SPLINE_SURFACE(2,2,((#125098,#125099,#125100),(#125101,#125102,#125103),
(#125104,#125105,#125106)),.UNSPECIFIED.,.F.,.F.,.F.)
B_SPLINE_SURFACE_WITH_KNOTS((3,3),(3,3),(-3.62708052714211E-14,1.57079632679498),
(-3.14159265358979,-1.57079632679461),.UNSPECIFIED.)
GEOMETRIC_REPRESENTATION_ITEM()
RATIONAL_B_SPLINE_SURFACE(((1.,0.707106781186447,1.),(0.707106781186491,
0.499999999999889,0.707106781186491),(1.,0.707106781186447,1.)))
REPRESENTATION_ITEM('')
SURFACE()
);
#60=(
BOUNDED_SURFACE()
B_SPLINE_SURFACE(2,2,((#125175,#125176,#125177),(#125178,#125179,#125180),
(#125181,#125182,#125183)),.UNSPECIFIED.,.F.,.F.,.F.)
B_SPLINE_SURFACE_WITH_KNOTS((3,3),(3,3),(-8.49689085742031E-14,1.57079632679491),
(-1.57076063039803,3.56963973534065E-5),.UNSPECIFIED.)
GEOMETRIC_REPRESENTATION_ITEM()
RATIONAL_B_SPLINE_SURFACE(((1.,0.707106781186375,1.),(0.707106781186495,
0.499999999999841,0.707106781186495),(1.,0.707106781186375,1.)))
REPRESENTATION_ITEM('')
SURFACE()
);
#61=(
BOUNDED_SURFACE()
B_SPLINE_SURFACE(2,2,((#125496,#125497,#125498),(#125499,#125500,#125501),
(#125502,#125503,#125504)),.UNSPECIFIED.,.F.,.F.,.F.)
B_SPLINE_SURFACE_WITH_KNOTS((3,3),(3,3),(-1.57079632679518,9.79900252594829E-15),
(-1.57076063039766,3.56963969770062E-5),.UNSPECIFIED.)
GEOMETRIC_REPRESENTATION_ITEM()
RATIONAL_B_SPLINE_SURFACE(((1.,0.707106781186639,1.),(0.70710678118645,
0.499999999999996,0.70710678118645),(1.,0.707106781186639,1.)))
REPRESENTATION_ITEM('')
SURFACE()
);
#62=(
BOUNDED_SURFACE()
B_SPLINE_SURFACE(2,2,((#125554,#125555,#125556),(#125557,#125558,#125559),
(#125560,#125561,#125562)),.UNSPECIFIED.,.F.,.F.,.F.)
B_SPLINE_SURFACE_WITH_KNOTS((3,3),(3,3),(-1.57079632679488,7.03247557642951E-14),
(-3.14159265358978,-1.57079632679492),.UNSPECIFIED.)
GEOMETRIC_REPRESENTATION_ITEM()
RATIONAL_B_SPLINE_SURFACE(((1.,0.707106781186562,1.),(0.707106781186541,
0.500000000000006,0.707106781186541),(1.,0.707106781186562,1.)))
REPRESENTATION_ITEM('')
SURFACE()
);
#79=TOROIDAL_SURFACE('',#28948,1.008,0.5);
#80=TOROIDAL_SURFACE('',#28954,2.5,0.5);
#81=TOROIDAL_SURFACE('',#28960,4.5,0.5);
#82=TOROIDAL_SURFACE('',#28975,1.49999999999999,0.5);
#83=TOROIDAL_SURFACE('',#28984,1.5,0.5);
#84=TOROIDAL_SURFACE('',#28999,4.5,0.5);
#85=TOROIDAL_SURFACE('',#29005,2.5,0.5);
#86=TOROIDAL_SURFACE('',#29011,1.008,0.5);
#87=TOROIDAL_SURFACE('',#29055,3.5,0.5);
#88=TOROIDAL_SURFACE('',#29066,3.5,0.5);
#89=TOROIDAL_SURFACE('',#29086,2.5,0.5);
#90=TOROIDAL_SURFACE('',#29094,4.5,0.5);
#91=TOROIDAL_SURFACE('',#29095,2.5,0.5);
#92=TOROIDAL_SURFACE('',#29101,1.5,0.5);
#93=TOROIDAL_SURFACE('',#29113,1.49999999999999,0.5);
#94=TOROIDAL_SURFACE('',#29119,4.5,0.5);
#107=ELLIPSE('',#28941,0.51530681467495,0.5);
#108=ELLIPSE('',#28970,0.541196100146195,0.5);
#109=ELLIPSE('',#28972,0.541196100146199,0.5);
#110=ELLIPSE('',#28980,0.515306814674945,0.5);
#111=ELLIPSE('',#28989,0.541196100146198,0.5);
#112=ELLIPSE('',#28991,0.541196100146195,0.5);
#113=ELLIPSE('',#29089,0.541196100146197,0.5);
#114=ELLIPSE('',#29097,0.541196100146196,0.5);
#115=ELLIPSE('',#29099,0.51530681467495,0.5);
#116=ELLIPSE('',#29105,0.515306814674951,0.5);
#117=ELLIPSE('',#29111,0.541196100146195,0.5);
#118=ELLIPSE('',#29118,0.541196100146198,0.5);
#202=FACE_BOUND('',#4876,.T.);
#203=FACE_BOUND('',#4931,.T.);
#1149=B_SPLINE_CURVE_WITH_KNOTS('',3,(#125335,#125336,#125337,#125338,#125339,
#125340,#125341,#125342,#125343,#125344,#125345,#125346,#125347,#125348),
 .UNSPECIFIED.,.F.,.F.,(4,2,2,2,2,2,4),(-0.000415314508948534,4.04163464848284E-15,
0.00908676885225018,0.0428529422967522,0.070010413556592,0.0906113630640777,
0.103462988684296),.UNSPECIFIED.);
#1150=B_SPLINE_CURVE_WITH_KNOTS('',3,(#125357,#125358,#125359,#125360,#125361,
#125362,#125363,#125364,#125365,#125366,#125367,#125368),.UNSPECIFIED.,
 .F.,.F.,(4,2,2,2,2,4),(-0.20607847627937,-0.203017141502583,-0.172677687898418,
-0.150776811472805,-0.13309642880445,-0.129817017892869),.UNSPECIFIED.);
#1151=B_SPLINE_CURVE_WITH_KNOTS('',3,(#125369,#125370,#125371,#125372,#125373,
#125374,#125375,#125376),.UNSPECIFIED.,.F.,.F.,(4,2,2,4),(-0.253933591178468,
-0.253367190412585,-0.22118528594891,-0.195623656529625),.UNSPECIFIED.);
#1152=B_SPLINE_CURVE_WITH_KNOTS('',3,(#125396,#125397,#125398,#125399,#125400,
#125401,#125402,#125403,#125404,#125405,#125406,#125407,#125408,#125409),
 .UNSPECIFIED.,.F.,.F.,(4,2,2,2,2,2,4),(-0.179602182967605,-0.179256977579029,
-0.171704143509864,-0.143638027894834,-0.121065001388135,-0.103941692120961,
-0.0932595456499447),.UNSPECIFIED.);
#1153=B_SPLINE_CURVE_WITH_KNOTS('',3,(#125413,#125414,#125415,#125416,#125417,
#125418,#125419,#125420),.UNSPECIFIED.,.F.,.F.,(4,2,2,4),(-0.049449650168343,
-0.0275595172389065,0.,0.000485046858821809),.UNSPECIFIED.);
#1154=B_SPLINE_CURVE_WITH_KNOTS('',3,(#125421,#125422,#125423,#125424,#125425,
#125426,#125427,#125428,#125429,#125430,#125431,#125432),.UNSPECIFIED.,
 .F.,.F.,(4,2,2,2,2,4),(-0.114326698231271,-0.111639541291989,-0.0971521945527792,
-0.0792065653985842,-0.0543463464492475,-0.0518378816027395),
 .UNSPECIFIED.);
#2123=SHAPE_REPRESENTATION_RELATIONSHIP('SRR','None',#215649,#2132);
#2132=ADVANCED_BREP_SHAPE_REPRESENTATION('',(#2150),#215605);
#2141=STYLED_ITEM('',(#215698),#2150);
#2150=MANIFOLD_SOLID_BREP('Body1',#28084);
#2506=CYLINDRICAL_SURFACE('',#28932,3.);
#2507=CYLINDRICAL_SURFACE('',#28936,3.);
#2508=CYLINDRICAL_SURFACE('',#28940,0.5);
#2509=CYLINDRICAL_SURFACE('',#28943,0.5);
#2510=CYLINDRICAL_SURFACE('',#28945,0.5);
#2511=CYLINDRICAL_SURFACE('',#28952,0.5);
#2512=CYLINDRICAL_SURFACE('',#28958,0.5);
#2513=CYLINDRICAL_SURFACE('',#28964,0.5);
#2514=CYLINDRICAL_SURFACE('',#28969,0.5);
#2515=CYLINDRICAL_SURFACE('',#28971,0.5);
#2516=CYLINDRICAL_SURFACE('',#28973,0.5);
#2517=CYLINDRICAL_SURFACE('',#28979,0.5);
#2518=CYLINDRICAL_SURFACE('',#28981,0.5);
#2519=CYLINDRICAL_SURFACE('',#28982,0.5);
#2520=CYLINDRICAL_SURFACE('',#28988,0.5);
#2521=CYLINDRICAL_SURFACE('',#28990,0.5);
#2522=CYLINDRICAL_SURFACE('',#28992,0.5);
#2523=CYLINDRICAL_SURFACE('',#28997,0.5);
#2524=CYLINDRICAL_SURFACE('',#29003,0.5);
#2525=CYLINDRICAL_SURFACE('',#29009,0.5);
#2526=CYLINDRICAL_SURFACE('',#29015,0.5);
#2527=CYLINDRICAL_SURFACE('',#29017,0.5);
#2528=CYLINDRICAL_SURFACE('',#29020,0.5);
#2529=CYLINDRICAL_SURFACE('',#29022,0.5);
#2530=CYLINDRICAL_SURFACE('',#29029,1.);
#2531=CYLINDRICAL_SURFACE('',#29034,1.);
#2532=CYLINDRICAL_SURFACE('',#29037,5.);
#2533=CYLINDRICAL_SURFACE('',#29040,3.);
#2534=CYLINDRICAL_SURFACE('',#29044,0.508000000000002);
#2535=CYLINDRICAL_SURFACE('',#29047,0.5);
#2536=CYLINDRICAL_SURFACE('',#29053,0.5);
#2537=CYLINDRICAL_SURFACE('',#29058,0.5);
#2538=CYLINDRICAL_SURFACE('',#29061,0.5);
#2539=CYLINDRICAL_SURFACE('',#29063,0.5);
#2540=CYLINDRICAL_SURFACE('',#29069,0.5);
#2541=CYLINDRICAL_SURFACE('',#29073,0.5);
#2542=CYLINDRICAL_SURFACE('',#29083,0.5);
#2543=CYLINDRICAL_SURFACE('',#29088,0.5);
#2544=CYLINDRICAL_SURFACE('',#29092,0.5);
#2545=CYLINDRICAL_SURFACE('',#29096,0.5);
#2546=CYLINDRICAL_SURFACE('',#29098,0.5);
#2547=CYLINDRICAL_SURFACE('',#29103,0.5);
#2548=CYLINDRICAL_SURFACE('',#29104,0.5);
#2549=CYLINDRICAL_SURFACE('',#29107,0.5);
#2550=CYLINDRICAL_SURFACE('',#29109,0.5);
#2551=CYLINDRICAL_SURFACE('',#29110,0.5);
#2552=CYLINDRICAL_SURFACE('',#29116,0.5);
#2553=CYLINDRICAL_SURFACE('',#29117,0.5);
#2554=CYLINDRICAL_SURFACE('',#29122,0.5);
#2555=CYLINDRICAL_SURFACE('',#29126,0.5);
#2556=CYLINDRICAL_SURFACE('',#29131,0.999999999999992);
#2557=CYLINDRICAL_SURFACE('',#29135,1.);
#2558=CYLINDRICAL_SURFACE('',#29137,5.);
#2559=CYLINDRICAL_SURFACE('',#29139,3.);
#2560=CYLINDRICAL_SURFACE('',#29141,3.);
#2561=CYLINDRICAL_SURFACE('',#29143,3.);
#2562=CYLINDRICAL_SURFACE('',#29149,0.508000000000002);
#2563=CYLINDRICAL_SURFACE('',#29151,0.499999999999998);
#3489=FACE_OUTER_BOUND('',#4831,.T.);
#3490=FACE_OUTER_BOUND('',#4832,.T.);
#3491=FACE_OUTER_BOUND('',#4833,.T.);
#3492=FACE_OUTER_BOUND('',#4834,.T.);
#3493=FACE_OUTER_BOUND('',#4835,.T.);
#3494=FACE_OUTER_BOUND('',#4836,.T.);
#3495=FACE_OUTER_BOUND('',#4837,.T.);
#3496=FACE_OUTER_BOUND('',#4838,.T.);
#3497=FACE_OUTER_BOUND('',#4839,.T.);
#3498=FACE_OUTER_BOUND('',#4840,.T.);
#3499=FACE_OUTER_BOUND('',#4841,.T.);
#3500=FACE_OUTER_BOUND('',#4842,.T.);
#3501=FACE_OUTER_BOUND('',#4843,.T.);
#3502=FACE_OUTER_BOUND('',#4844,.T.);
#3503=FACE_OUTER_BOUND('',#4845,.T.);
#3504=FACE_OUTER_BOUND('',#4846,.T.);
#3505=FACE_OUTER_BOUND('',#4847,.T.);
#3506=FACE_OUTER_BOUND('',#4848,.T.);
#3507=FACE_OUTER_BOUND('',#4849,.T.);
#3508=FACE_OUTER_BOUND('',#4850,.T.);
#3509=FACE_OUTER_BOUND('',#4851,.T.);
#3510=FACE_OUTER_BOUND('',#4852,.T.);
#3511=FACE_OUTER_BOUND('',#4853,.T.);
#3512=FACE_OUTER_BOUND('',#4854,.T.);
#3513=FACE_OUTER_BOUND('',#4855,.T.);
#3514=FACE_OUTER_BOUND('',#4856,.T.);
#3515=FACE_OUTER_BOUND('',#4857,.T.);
#3516=FACE_OUTER_BOUND('',#4858,.T.);
#3517=FACE_OUTER_BOUND('',#4859,.T.);
#3518=FACE_OUTER_BOUND('',#4860,.T.);
#3519=FACE_OUTER_BOUND('',#4861,.T.);
#3520=FACE_OUTER_BOUND('',#4862,.T.);
#3521=FACE_OUTER_BOUND('',#4863,.T.);
#3522=FACE_OUTER_BOUND('',#4864,.T.);
#3523=FACE_OUTER_BOUND('',#4865,.T.);
#3524=FACE_OUTER_BOUND('',#4866,.T.);
#3525=FACE_OUTER_BOUND('',#4867,.T.);
#3526=FACE_OUTER_BOUND('',#4868,.T.);
#3527=FACE_OUTER_BOUND('',#4869,.T.);
#3528=FACE_OUTER_BOUND('',#4870,.T.);
#3529=FACE_OUTER_BOUND('',#4871,.T.);
#3530=FACE_OUTER_BOUND('',#4872,.T.);
#3531=FACE_OUTER_BOUND('',#4873,.T.);
#3532=FACE_OUTER_BOUND('',#4874,.T.);
#3533=FACE_OUTER_BOUND('',#4875,.T.);
#3534=FACE_OUTER_BOUND('',#4877,.T.);
#3535=FACE_OUTER_BOUND('',#4878,.T.);
#3536=FACE_OUTER_BOUND('',#4879,.T.);
#3537=FACE_OUTER_BOUND('',#4880,.T.);
#3538=FACE_OUTER_BOUND('',#4881,.T.);
#3539=FACE_OUTER_BOUND('',#4882,.T.);
#3540=FACE_OUTER_BOUND('',#4883,.T.);
#3541=FACE_OUTER_BOUND('',#4884,.T.);
#3542=FACE_OUTER_BOUND('',#4885,.T.);
#3543=FACE_OUTER_BOUND('',#4886,.T.);
#3544=FACE_OUTER_BOUND('',#4887,.T.);
#3545=FACE_OUTER_BOUND('',#4888,.T.);
#3546=FACE_OUTER_BOUND('',#4889,.T.);
#3547=FACE_OUTER_BOUND('',#4890,.T.);
#3548=FACE_OUTER_BOUND('',#4891,.T.);
#3549=FACE_OUTER_BOUND('',#4892,.T.);
#3550=FACE_OUTER_BOUND('',#4893,.T.);
#3551=FACE_OUTER_BOUND('',#4894,.T.);
#3552=FACE_OUTER_BOUND('',#4895,.T.);
#3553=FACE_OUTER_BOUND('',#4896,.T.);
#3554=FACE_OUTER_BOUND('',#4897,.T.);
#3555=FACE_OUTER_BOUND('',#4898,.T.);
#3556=FACE_OUTER_BOUND('',#4899,.T.);
#3557=FACE_OUTER_BOUND('',#4900,.T.);
#3558=FACE_OUTER_BOUND('',#4901,.T.);
#3559=FACE_OUTER_BOUND('',#4902,.T.);
#3560=FACE_OUTER_BOUND('',#4903,.T.);
#3561=FACE_OUTER_BOUND('',#4904,.T.);
#3562=FACE_OUTER_BOUND('',#4905,.T.);
#3563=FACE_OUTER_BOUND('',#4906,.T.);
#3564=FACE_OUTER_BOUND('',#4907,.T.);
#3565=FACE_OUTER_BOUND('',#4908,.T.);
#3566=FACE_OUTER_BOUND('',#4909,.T.);
#3567=FACE_OUTER_BOUND('',#4910,.T.);
#3568=FACE_OUTER_BOUND('',#4911,.T.);
#3569=FACE_OUTER_BOUND('',#4912,.T.);
#3570=FACE_OUTER_BOUND('',#4913,.T.);
#3571=FACE_OUTER_BOUND('',#4914,.T.);
#3572=FACE_OUTER_BOUND('',#4915,.T.);
#3573=FACE_OUTER_BOUND('',#4916,.T.);
#3574=FACE_OUTER_BOUND('',#4917,.T.);
#3575=FACE_OUTER_BOUND('',#4918,.T.);
#3576=FACE_OUTER_BOUND('',#4919,.T.);
#3577=FACE_OUTER_BOUND('',#4920,.T.);
#3578=FACE_OUTER_BOUND('',#4921,.T.);
#3579=FACE_OUTER_BOUND('',#4922,.T.);
#3580=FACE_OUTER_BOUND('',#4923,.T.);
#3581=FACE_OUTER_BOUND('',#4924,.T.);
#3582=FACE_OUTER_BOUND('',#4925,.T.);
#3583=FACE_OUTER_BOUND('',#4926,.T.);
#3584=FACE_OUTER_BOUND('',#4927,.T.);
#3585=FACE_OUTER_BOUND('',#4928,.T.);
#3586=FACE_OUTER_BOUND('',#4929,.T.);
#3587=FACE_OUTER_BOUND('',#4930,.T.);
#3588=FACE_OUTER_BOUND('',#4932,.T.);
#3589=FACE_OUTER_BOUND('',#4933,.T.);
#3590=FACE_OUTER_BOUND('',#4934,.T.);
#3591=FACE_OUTER_BOUND('',#4935,.T.);
#3592=FACE_OUTER_BOUND('',#4936,.T.);
#3593=FACE_OUTER_BOUND('',#4937,.T.);
#3594=FACE_OUTER_BOUND('',#4938,.T.);
#3595=FACE_OUTER_BOUND('',#4939,.T.);
#3596=FACE_OUTER_BOUND('',#4940,.T.);
#3597=FACE_OUTER_BOUND('',#4941,.T.);
#3598=FACE_OUTER_BOUND('',#4942,.T.);
#4831=EDGE_LOOP('',(#21137,#21138,#21139,#21140));
#4832=EDGE_LOOP('',(#21141));
#4833=EDGE_LOOP('',(#21142,#21143,#21144,#21145));
#4834=EDGE_LOOP('',(#21146));
#4835=EDGE_LOOP('',(#21147,#21148,#21149,#21150));
#4836=EDGE_LOOP('',(#21151,#21152,#21153,#21154));
#4837=EDGE_LOOP('',(#21155,#21156,#21157,#21158));
#4838=EDGE_LOOP('',(#21159,#21160,#21161,#21162));
#4839=EDGE_LOOP('',(#21163,#21164,#21165,#21166));
#4840=EDGE_LOOP('',(#21167,#21168,#21169,#21170));
#4841=EDGE_LOOP('',(#21171,#21172,#21173,#21174));
#4842=EDGE_LOOP('',(#21175,#21176,#21177,#21178));
#4843=EDGE_LOOP('',(#21179,#21180,#21181,#21182));
#4844=EDGE_LOOP('',(#21183,#21184,#21185,#21186));
#4845=EDGE_LOOP('',(#21187,#21188,#21189,#21190));
#4846=EDGE_LOOP('',(#21191,#21192,#21193,#21194));
#4847=EDGE_LOOP('',(#21195,#21196,#21197,#21198));
#4848=EDGE_LOOP('',(#21199,#21200,#21201,#21202));
#4849=EDGE_LOOP('',(#21203,#21204,#21205,#21206));
#4850=EDGE_LOOP('',(#21207,#21208,#21209,#21210));
#4851=EDGE_LOOP('',(#21211,#21212,#21213,#21214));
#4852=EDGE_LOOP('',(#21215,#21216,#21217,#21218));
#4853=EDGE_LOOP('',(#21219,#21220,#21221,#21222));
#4854=EDGE_LOOP('',(#21223,#21224,#21225,#21226));
#4855=EDGE_LOOP('',(#21227,#21228,#21229,#21230));
#4856=EDGE_LOOP('',(#21231,#21232,#21233,#21234));
#4857=EDGE_LOOP('',(#21235,#21236,#21237,#21238));
#4858=EDGE_LOOP('',(#21239,#21240,#21241,#21242));
#4859=EDGE_LOOP('',(#21243,#21244,#21245,#21246));
#4860=EDGE_LOOP('',(#21247,#21248,#21249,#21250));
#4861=EDGE_LOOP('',(#21251,#21252,#21253,#21254));
#4862=EDGE_LOOP('',(#21255,#21256,#21257,#21258));
#4863=EDGE_LOOP('',(#21259,#21260,#21261,#21262));
#4864=EDGE_LOOP('',(#21263,#21264,#21265,#21266));
#4865=EDGE_LOOP('',(#21267,#21268,#21269,#21270));
#4866=EDGE_LOOP('',(#21271,#21272,#21273,#21274));
#4867=EDGE_LOOP('',(#21275,#21276,#21277));
#4868=EDGE_LOOP('',(#21278,#21279,#21280));
#4869=EDGE_LOOP('',(#21281,#21282,#21283,#21284));
#4870=EDGE_LOOP('',(#21285,#21286,#21287,#21288));
#4871=EDGE_LOOP('',(#21289,#21290,#21291,#21292));
#4872=EDGE_LOOP('',(#21293,#21294,#21295,#21296));
#4873=EDGE_LOOP('',(#21297,#21298,#21299,#21300));
#4874=EDGE_LOOP('',(#21301,#21302,#21303,#21304));
#4875=EDGE_LOOP('',(#21305,#21306,#21307,#21308));
#4876=EDGE_LOOP('',(#21309));
#4877=EDGE_LOOP('',(#21310,#21311,#21312,#21313));
#4878=EDGE_LOOP('',(#21314,#21315,#21316,#21317));
#4879=EDGE_LOOP('',(#21318,#21319,#21320,#21321,#21322,#21323));
#4880=EDGE_LOOP('',(#21324,#21325,#21326,#21327));
#4881=EDGE_LOOP('',(#21328,#21329,#21330,#21331));
#4882=EDGE_LOOP('',(#21332,#21333,#21334,#21335,#21336,#21337));
#4883=EDGE_LOOP('',(#21338,#21339,#21340,#21341));
#4884=EDGE_LOOP('',(#21342,#21343,#21344,#21345));
#4885=EDGE_LOOP('',(#21346,#21347,#21348,#21349));
#4886=EDGE_LOOP('',(#21350,#21351,#21352,#21353));
#4887=EDGE_LOOP('',(#21354,#21355,#21356,#21357,#21358,#21359,#21360,#21361,
#21362,#21363,#21364,#21365,#21366,#21367,#21368,#21369,#21370,#21371,#21372,
#21373,#21374,#21375,#21376,#21377,#21378,#21379,#21380,#21381,#21382,#21383,
#21384,#21385));
#4888=EDGE_LOOP('',(#21386,#21387,#21388,#21389));
#4889=EDGE_LOOP('',(#21390,#21391,#21392,#21393,#21394));
#4890=EDGE_LOOP('',(#21395,#21396,#21397,#21398));
#4891=EDGE_LOOP('',(#21399,#21400,#21401,#21402));
#4892=EDGE_LOOP('',(#21403,#21404,#21405,#21406));
#4893=EDGE_LOOP('',(#21407,#21408,#21409));
#4894=EDGE_LOOP('',(#21410,#21411,#21412,#21413,#21414));
#4895=EDGE_LOOP('',(#21415,#21416,#21417,#21418));
#4896=EDGE_LOOP('',(#21419,#21420,#21421));
#4897=EDGE_LOOP('',(#21422,#21423,#21424,#21425,#21426));
#4898=EDGE_LOOP('',(#21427,#21428,#21429,#21430,#21431,#21432,#21433,#21434,
#21435,#21436,#21437,#21438,#21439,#21440,#21441,#21442,#21443,#21444,#21445,
#21446,#21447,#21448,#21449,#21450,#21451,#21452,#21453,#21454));
#4899=EDGE_LOOP('',(#21455,#21456,#21457,#21458,#21459));
#4900=EDGE_LOOP('',(#21460,#21461,#21462));
#4901=EDGE_LOOP('',(#21463,#21464,#21465,#21466));
#4902=EDGE_LOOP('',(#21467,#21468,#21469,#21470));
#4903=EDGE_LOOP('',(#21471,#21472,#21473,#21474));
#4904=EDGE_LOOP('',(#21475,#21476,#21477,#21478));
#4905=EDGE_LOOP('',(#21479,#21480,#21481));
#4906=EDGE_LOOP('',(#21482,#21483,#21484,#21485));
#4907=EDGE_LOOP('',(#21486,#21487,#21488,#21489));
#4908=EDGE_LOOP('',(#21490,#21491,#21492,#21493));
#4909=EDGE_LOOP('',(#21494,#21495,#21496,#21497));
#4910=EDGE_LOOP('',(#21498,#21499,#21500,#21501));
#4911=EDGE_LOOP('',(#21502,#21503,#21504,#21505));
#4912=EDGE_LOOP('',(#21506,#21507,#21508,#21509));
#4913=EDGE_LOOP('',(#21510,#21511,#21512,#21513));
#4914=EDGE_LOOP('',(#21514,#21515,#21516,#21517));
#4915=EDGE_LOOP('',(#21518,#21519,#21520,#21521));
#4916=EDGE_LOOP('',(#21522,#21523,#21524,#21525));
#4917=EDGE_LOOP('',(#21526,#21527,#21528,#21529));
#4918=EDGE_LOOP('',(#21530,#21531,#21532,#21533));
#4919=EDGE_LOOP('',(#21534,#21535,#21536,#21537));
#4920=EDGE_LOOP('',(#21538,#21539,#21540,#21541));
#4921=EDGE_LOOP('',(#21542,#21543,#21544,#21545));
#4922=EDGE_LOOP('',(#21546,#21547,#21548,#21549));
#4923=EDGE_LOOP('',(#21550,#21551,#21552,#21553));
#4924=EDGE_LOOP('',(#21554,#21555,#21556,#21557));
#4925=EDGE_LOOP('',(#21558,#21559,#21560,#21561));
#4926=EDGE_LOOP('',(#21562,#21563,#21564,#21565));
#4927=EDGE_LOOP('',(#21566,#21567,#21568,#21569));
#4928=EDGE_LOOP('',(#21570,#21571,#21572,#21573));
#4929=EDGE_LOOP('',(#21574,#21575,#21576,#21577));
#4930=EDGE_LOOP('',(#21578,#21579,#21580,#21581));
#4931=EDGE_LOOP('',(#21582));
#4932=EDGE_LOOP('',(#21583,#21584,#21585,#21586));
#4933=EDGE_LOOP('',(#21587,#21588,#21589,#21590));
#4934=EDGE_LOOP('',(#21591,#21592,#21593,#21594,#21595,#21596));
#4935=EDGE_LOOP('',(#21597,#21598,#21599,#21600));
#4936=EDGE_LOOP('',(#21601,#21602,#21603,#21604));
#4937=EDGE_LOOP('',(#21605,#21606,#21607,#21608,#21609));
#4938=EDGE_LOOP('',(#21610,#21611,#21612,#21613,#21614));
#4939=EDGE_LOOP('',(#21615,#21616,#21617,#21618));
#4940=EDGE_LOOP('',(#21619,#21620,#21621,#21622));
#4941=EDGE_LOOP('',(#21623,#21624,#21625,#21626,#21627,#21628));
#4942=EDGE_LOOP('',(#21629,#21630,#21631,#21632));
#5890=CIRCLE('',#28933,3.);
#5891=CIRCLE('',#28934,3.);
#5892=CIRCLE('',#28937,3.);
#5893=CIRCLE('',#28938,3.);
#5894=CIRCLE('',#28942,0.499999999999998);
#5895=CIRCLE('',#28944,0.499999999999999);
#5896=CIRCLE('',#28946,0.5);
#5897=CIRCLE('',#28947,0.499999999999998);
#5898=CIRCLE('',#28949,0.499999999999998);
#5899=CIRCLE('',#28950,1.008);
#5900=CIRCLE('',#28951,0.508000000000002);
#5901=CIRCLE('',#28953,0.499999999999998);
#5902=CIRCLE('',#28955,0.499999999999998);
#5903=CIRCLE('',#28956,2.5);
#5904=CIRCLE('',#28957,3.);
#5905=CIRCLE('',#28959,0.499999999999998);
#5906=CIRCLE('',#28961,0.499999999999998);
#5907=CIRCLE('',#28962,4.5);
#5908=CIRCLE('',#28963,5.);
#5909=CIRCLE('',#28965,0.499999999999998);
#5910=CIRCLE('',#28966,0.499999999999998);
#5911=CIRCLE('',#28967,0.500000000000001);
#5912=CIRCLE('',#28968,1.);
#5913=CIRCLE('',#28974,0.499999999999998);
#5914=CIRCLE('',#28976,0.499999999999998);
#5915=CIRCLE('',#28977,1.49999999999999);
#5916=CIRCLE('',#28978,0.999999999999992);
#5917=CIRCLE('',#28983,0.499999999999998);
#5918=CIRCLE('',#28985,0.499999999999998);
#5919=CIRCLE('',#28986,1.5);
#5920=CIRCLE('',#28987,1.);
#5921=CIRCLE('',#28993,0.499999999999998);
#5922=CIRCLE('',#28994,0.499999999999998);
#5923=CIRCLE('',#28995,0.5);
#5924=CIRCLE('',#28996,1.);
#5925=CIRCLE('',#28998,0.499999999999998);
#5926=CIRCLE('',#29000,0.499999999999998);
#5927=CIRCLE('',#29001,4.5);
#5928=CIRCLE('',#29002,5.);
#5929=CIRCLE('',#29004,0.499999999999998);
#5930=CIRCLE('',#29006,0.499999999999998);
#5931=CIRCLE('',#29007,2.5);
#5932=CIRCLE('',#29008,3.);
#5933=CIRCLE('',#29010,0.499999999999998);
#5934=CIRCLE('',#29012,0.499999999999998);
#5935=CIRCLE('',#29013,1.008);
#5936=CIRCLE('',#29014,0.508000000000002);
#5937=CIRCLE('',#29016,0.499999999999998);
#5938=CIRCLE('',#29018,0.499999999999998);
#5939=CIRCLE('',#29019,0.499999999999998);
#5940=CIRCLE('',#29021,0.500000000000004);
#5941=CIRCLE('',#29023,0.499999999999993);
#5942=CIRCLE('',#29025,0.5);
#5943=CIRCLE('',#29027,0.499999999999998);
#5944=CIRCLE('',#29030,1.);
#5945=CIRCLE('',#29035,1.);
#5946=CIRCLE('',#29038,5.);
#5947=CIRCLE('',#29041,3.);
#5948=CIRCLE('',#29042,3.);
#5949=CIRCLE('',#29045,0.508000000000002);
#5950=CIRCLE('',#29048,0.5);
#5951=CIRCLE('',#29054,0.5);
#5952=CIRCLE('',#29056,3.5);
#5953=CIRCLE('',#29057,3.);
#5954=CIRCLE('',#29059,0.500000000000002);
#5955=CIRCLE('',#29060,0.5);
#5956=CIRCLE('',#29062,0.500000000000004);
#5957=CIRCLE('',#29064,0.499999999999998);
#5958=CIRCLE('',#29067,3.);
#5959=CIRCLE('',#29068,3.5);
#5960=CIRCLE('',#29070,0.5);
#5961=CIRCLE('',#29072,0.499999999999998);
#5962=CIRCLE('',#29074,0.500000000000001);
#5963=CIRCLE('',#29075,0.499999999999998);
#5964=CIRCLE('',#29077,4.5);
#5965=CIRCLE('',#29078,0.5);
#5966=CIRCLE('',#29079,1.5);
#5967=CIRCLE('',#29080,1.49999999999999);
#5968=CIRCLE('',#29081,0.500000000000001);
#5969=CIRCLE('',#29082,4.5);
#5970=CIRCLE('',#29084,0.499999999999999);
#5971=CIRCLE('',#29085,0.499999999999999);
#5972=CIRCLE('',#29087,3.);
#5973=CIRCLE('',#29090,0.5);
#5974=CIRCLE('',#29091,0.500000000000002);
#5975=CIRCLE('',#29093,0.499999999999998);
#5976=CIRCLE('',#29100,0.499999999999995);
#5977=CIRCLE('',#29102,0.5);
#5978=CIRCLE('',#29106,0.499999999999998);
#5979=CIRCLE('',#29108,0.499999999999999);
#5980=CIRCLE('',#29112,0.5);
#5981=CIRCLE('',#29114,0.500000000000001);
#5982=CIRCLE('',#29115,0.999999999999992);
#5983=CIRCLE('',#29120,0.499999999999998);
#5984=CIRCLE('',#29121,5.);
#5985=CIRCLE('',#29123,0.499999999999998);
#5986=CIRCLE('',#29124,0.5);
#5987=CIRCLE('',#29125,1.);
#5988=CIRCLE('',#29140,3.);
#5989=CIRCLE('',#29142,3.);
#5990=CIRCLE('',#29144,3.);
#5991=CIRCLE('',#29147,0.508000000000002);
#6960=LINE('',#125028,#8805);
#6961=LINE('',#125035,#8806);
#6962=LINE('',#125041,#8807);
#6963=LINE('',#125045,#8808);
#6964=LINE('',#125049,#8809);
#6965=LINE('',#125052,#8810);
#6966=LINE('',#125058,#8811);
#6967=LINE('',#125061,#8812);
#6968=LINE('',#125072,#8813);
#6969=LINE('',#125073,#8814);
#6970=LINE('',#125084,#8815);
#6971=LINE('',#125085,#8816);
#6972=LINE('',#125096,#8817);
#6973=LINE('',#125097,#8818);
#6974=LINE('',#125114,#8819);
#6975=LINE('',#125117,#8820);
#6976=LINE('',#125120,#8821);
#6977=LINE('',#125123,#8822);
#6978=LINE('',#125126,#8823);
#6979=LINE('',#125128,#8824);
#6980=LINE('',#125138,#8825);
#6981=LINE('',#125141,#8826);
#6982=LINE('',#125143,#8827);
#6983=LINE('',#125144,#8828);
#6984=LINE('',#125147,#8829);
#6985=LINE('',#125149,#8830);
#6986=LINE('',#125159,#8831);
#6987=LINE('',#125162,#8832);
#6988=LINE('',#125165,#8833);
#6989=LINE('',#125167,#8834);
#6990=LINE('',#125171,#8835);
#6991=LINE('',#125173,#8836);
#6992=LINE('',#125193,#8837);
#6993=LINE('',#125194,#8838);
#6994=LINE('',#125205,#8839);
#6995=LINE('',#125206,#8840);
#6996=LINE('',#125217,#8841);
#6997=LINE('',#125218,#8842);
#6998=LINE('',#125229,#8843);
#6999=LINE('',#125230,#8844);
#7000=LINE('',#125236,#8845);
#7001=LINE('',#125238,#8846);
#7002=LINE('',#125241,#8847);
#7003=LINE('',#125244,#8848);
#7004=LINE('',#125246,#8849);
#7005=LINE('',#125249,#8850);
#7006=LINE('',#125256,#8851);
#7007=LINE('',#125258,#8852);
#7008=LINE('',#125259,#8853);
#7009=LINE('',#125263,#8854);
#7010=LINE('',#125266,#8855);
#7011=LINE('',#125267,#8856);
#7012=LINE('',#125270,#8857);
#7013=LINE('',#125271,#8858);
#7014=LINE('',#125274,#8859);
#7015=LINE('',#125275,#8860);
#7016=LINE('',#125279,#8861);
#7017=LINE('',#125282,#8862);
#7018=LINE('',#125283,#8863);
#7019=LINE('',#125287,#8864);
#7020=LINE('',#125290,#8865);
#7021=LINE('',#125291,#8866);
#7022=LINE('',#125296,#8867);
#7023=LINE('',#125299,#8868);
#7024=LINE('',#125302,#8869);
#7025=LINE('',#125303,#8870);
#7026=LINE('',#125307,#8871);
#7027=LINE('',#125310,#8872);
#7028=LINE('',#125312,#8873);
#7029=LINE('',#125314,#8874);
#7030=LINE('',#125315,#8875);
#7031=LINE('',#125319,#8876);
#7032=LINE('',#125322,#8877);
#7033=LINE('',#125323,#8878);
#7034=LINE('',#125326,#8879);
#7035=LINE('',#125327,#8880);
#7036=LINE('',#125330,#8881);
#7037=LINE('',#125331,#8882);
#7038=LINE('',#125350,#8883);
#7039=LINE('',#125381,#8884);
#7040=LINE('',#125385,#8885);
#7041=LINE('',#125388,#8886);
#7042=LINE('',#125434,#8887);
#7043=LINE('',#125436,#8888);
#7044=LINE('',#125444,#8889);
#7045=LINE('',#125449,#8890);
#7046=LINE('',#125453,#8891);
#7047=LINE('',#125455,#8892);
#7048=LINE('',#125457,#8893);
#7049=LINE('',#125461,#8894);
#7050=LINE('',#125463,#8895);
#7051=LINE('',#125465,#8896);
#7052=LINE('',#125467,#8897);
#7053=LINE('',#125469,#8898);
#7054=LINE('',#125473,#8899);
#7055=LINE('',#125475,#8900);
#7056=LINE('',#125477,#8901);
#7057=LINE('',#125481,#8902);
#7058=LINE('',#125484,#8903);
#7059=LINE('',#125489,#8904);
#7060=LINE('',#125521,#8905);
#7061=LINE('',#125527,#8906);
#7062=LINE('',#125529,#8907);
#7063=LINE('',#125533,#8908);
#7064=LINE('',#125541,#8909);
#7065=LINE('',#125544,#8910);
#7066=LINE('',#125553,#8911);
#7067=LINE('',#125567,#8912);
#7068=LINE('',#125569,#8913);
#7069=LINE('',#125571,#8914);
#7070=LINE('',#125573,#8915);
#7071=LINE('',#125575,#8916);
#7072=LINE('',#125577,#8917);
#7073=LINE('',#125579,#8918);
#7074=LINE('',#125581,#8919);
#7075=LINE('',#125583,#8920);
#7076=LINE('',#125585,#8921);
#7077=LINE('',#125587,#8922);
#7078=LINE('',#125589,#8923);
#7079=LINE('',#125591,#8924);
#7080=LINE('',#125594,#8925);
#7081=LINE('',#125597,#8926);
#7082=LINE('',#125601,#8927);
#7083=LINE('',#125607,#8928);
#7084=LINE('',#125610,#8929);
#7085=LINE('',#125612,#8930);
#7086=LINE('',#125614,#8931);
#7087=LINE('',#125616,#8932);
#8805=VECTOR('',#32340,3.);
#8806=VECTOR('',#32349,3.);
#8807=VECTOR('',#32356,10.);
#8808=VECTOR('',#32359,10.);
#8809=VECTOR('',#32364,10.);
#8810=VECTOR('',#32367,10.);
#8811=VECTOR('',#32372,10.);
#8812=VECTOR('',#32375,10.);
#8813=VECTOR('',#32388,10.);
#8814=VECTOR('',#32389,10.);
#8815=VECTOR('',#32402,10.);
#8816=VECTOR('',#32403,10.);
#8817=VECTOR('',#32416,10.);
#8818=VECTOR('',#32417,10.);
#8819=VECTOR('',#32426,10.);
#8820=VECTOR('',#32429,10.);
#8821=VECTOR('',#32432,10.);
#8822=VECTOR('',#32435,10.);
#8823=VECTOR('',#32438,10.);
#8824=VECTOR('',#32439,10.);
#8825=VECTOR('',#32452,10.);
#8826=VECTOR('',#32455,10.);
#8827=VECTOR('',#32458,10.);
#8828=VECTOR('',#32459,10.);
#8829=VECTOR('',#32462,10.);
#8830=VECTOR('',#32463,10.);
#8831=VECTOR('',#32476,10.);
#8832=VECTOR('',#32479,10.);
#8833=VECTOR('',#32482,10.);
#8834=VECTOR('',#32483,10.);
#8835=VECTOR('',#32488,10.);
#8836=VECTOR('',#32489,10.);
#8837=VECTOR('',#32502,10.);
#8838=VECTOR('',#32503,10.);
#8839=VECTOR('',#32516,10.);
#8840=VECTOR('',#32517,10.);
#8841=VECTOR('',#32530,10.);
#8842=VECTOR('',#32531,10.);
#8843=VECTOR('',#32544,10.);
#8844=VECTOR('',#32545,10.);
#8845=VECTOR('',#32550,10.);
#8846=VECTOR('',#32553,10.);
#8847=VECTOR('',#32556,10.);
#8848=VECTOR('',#32559,10.);
#8849=VECTOR('',#32562,10.);
#8850=VECTOR('',#32565,10.);
#8851=VECTOR('',#32576,10.);
#8852=VECTOR('',#32577,10.);
#8853=VECTOR('',#32578,10.);
#8854=VECTOR('',#32583,10.);
#8855=VECTOR('',#32586,10.);
#8856=VECTOR('',#32587,10.);
#8857=VECTOR('',#32590,10.);
#8858=VECTOR('',#32591,10.);
#8859=VECTOR('',#32594,10.);
#8860=VECTOR('',#32595,10.);
#8861=VECTOR('',#32600,10.);
#8862=VECTOR('',#32603,10.);
#8863=VECTOR('',#32604,10.);
#8864=VECTOR('',#32609,10.);
#8865=VECTOR('',#32612,10.);
#8866=VECTOR('',#32613,10.);
#8867=VECTOR('',#32618,10.);
#8868=VECTOR('',#32621,10.);
#8869=VECTOR('',#32624,10.);
#8870=VECTOR('',#32625,10.);
#8871=VECTOR('',#32630,10.);
#8872=VECTOR('',#32633,10.);
#8873=VECTOR('',#32634,10.);
#8874=VECTOR('',#32635,10.);
#8875=VECTOR('',#32636,10.);
#8876=VECTOR('',#32641,10.);
#8877=VECTOR('',#32644,10.);
#8878=VECTOR('',#32645,10.);
#8879=VECTOR('',#32648,10.);
#8880=VECTOR('',#32649,10.);
#8881=VECTOR('',#32652,10.);
#8882=VECTOR('',#32653,10.);
#8883=VECTOR('',#32658,10.);
#8884=VECTOR('',#32673,10.);
#8885=VECTOR('',#32678,10.);
#8886=VECTOR('',#32681,10.);
#8887=VECTOR('',#32694,10.);
#8888=VECTOR('',#32695,10.);
#8889=VECTOR('',#32708,10.);
#8890=VECTOR('',#32713,10.);
#8891=VECTOR('',#32716,10.);
#8892=VECTOR('',#32717,10.);
#8893=VECTOR('',#32718,10.);
#8894=VECTOR('',#32721,10.);
#8895=VECTOR('',#32722,10.);
#8896=VECTOR('',#32723,10.);
#8897=VECTOR('',#32724,10.);
#8898=VECTOR('',#32725,10.);
#8899=VECTOR('',#32728,10.);
#8900=VECTOR('',#32729,10.);
#8901=VECTOR('',#32730,10.);
#8902=VECTOR('',#32733,10.);
#8903=VECTOR('',#32736,10.);
#8904=VECTOR('',#32741,10.);
#8905=VECTOR('',#32782,10.);
#8906=VECTOR('',#32791,10.);
#8907=VECTOR('',#32794,10.);
#8908=VECTOR('',#32797,10.);
#8909=VECTOR('',#32810,10.);
#8910=VECTOR('',#32813,10.);
#8911=VECTOR('',#32826,10.);
#8912=VECTOR('',#32833,10.);
#8913=VECTOR('',#32836,10.);
#8914=VECTOR('',#32839,10.);
#8915=VECTOR('',#32842,10.);
#8916=VECTOR('',#32845,10.);
#8917=VECTOR('',#32848,10.);
#8918=VECTOR('',#32851,10.);
#8919=VECTOR('',#32854,10.);
#8920=VECTOR('',#32857,10.);
#8921=VECTOR('',#32860,10.);
#8922=VECTOR('',#32863,10.);
#8923=VECTOR('',#32866,10.);
#8924=VECTOR('',#32869,10.);
#8925=VECTOR('',#32872,10.);
#8926=VECTOR('',#32875,10.);
#8927=VECTOR('',#32880,10.);
#8928=VECTOR('',#32889,10.);
#8929=VECTOR('',#32892,10.);
#8930=VECTOR('',#32895,10.);
#8931=VECTOR('',#32898,10.);
#8932=VECTOR('',#32901,10.);
#11294=VERTEX_POINT('',#125025);
#11295=VERTEX_POINT('',#125027);
#11296=VERTEX_POINT('',#125032);
#11297=VERTEX_POINT('',#125034);
#11298=VERTEX_POINT('',#125039);
#11299=VERTEX_POINT('',#125040);
#11300=VERTEX_POINT('',#125042);
#11301=VERTEX_POINT('',#125044);
#11302=VERTEX_POINT('',#125048);
#11303=VERTEX_POINT('',#125050);
#11304=VERTEX_POINT('',#125054);
#11305=VERTEX_POINT('',#125055);
#11306=VERTEX_POINT('',#125057);
#11307=VERTEX_POINT('',#125059);
#11308=VERTEX_POINT('',#125063);
#11309=VERTEX_POINT('',#125064);
#11310=VERTEX_POINT('',#125069);
#11311=VERTEX_POINT('',#125070);
#11312=VERTEX_POINT('',#125075);
#11313=VERTEX_POINT('',#125076);
#11314=VERTEX_POINT('',#125081);
#11315=VERTEX_POINT('',#125082);
#11316=VERTEX_POINT('',#125087);
#11317=VERTEX_POINT('',#125088);
#11318=VERTEX_POINT('',#125093);
#11319=VERTEX_POINT('',#125094);
#11320=VERTEX_POINT('',#125107);
#11321=VERTEX_POINT('',#125108);
#11322=VERTEX_POINT('',#125113);
#11323=VERTEX_POINT('',#125115);
#11324=VERTEX_POINT('',#125119);
#11325=VERTEX_POINT('',#125121);
#11326=VERTEX_POINT('',#125125);
#11327=VERTEX_POINT('',#125127);
#11328=VERTEX_POINT('',#125131);
#11329=VERTEX_POINT('',#125132);
#11330=VERTEX_POINT('',#125137);
#11331=VERTEX_POINT('',#125139);
#11332=VERTEX_POINT('',#125146);
#11333=VERTEX_POINT('',#125148);
#11334=VERTEX_POINT('',#125152);
#11335=VERTEX_POINT('',#125153);
#11336=VERTEX_POINT('',#125158);
#11337=VERTEX_POINT('',#125160);
#11338=VERTEX_POINT('',#125164);
#11339=VERTEX_POINT('',#125166);
#11340=VERTEX_POINT('',#125170);
#11341=VERTEX_POINT('',#125172);
#11342=VERTEX_POINT('',#125184);
#11343=VERTEX_POINT('',#125185);
#11344=VERTEX_POINT('',#125190);
#11345=VERTEX_POINT('',#125191);
#11346=VERTEX_POINT('',#125196);
#11347=VERTEX_POINT('',#125197);
#11348=VERTEX_POINT('',#125202);
#11349=VERTEX_POINT('',#125203);
#11350=VERTEX_POINT('',#125208);
#11351=VERTEX_POINT('',#125209);
#11352=VERTEX_POINT('',#125214);
#11353=VERTEX_POINT('',#125215);
#11354=VERTEX_POINT('',#125220);
#11355=VERTEX_POINT('',#125221);
#11356=VERTEX_POINT('',#125226);
#11357=VERTEX_POINT('',#125227);
#11358=VERTEX_POINT('',#125232);
#11359=VERTEX_POINT('',#125233);
#11360=VERTEX_POINT('',#125235);
#11361=VERTEX_POINT('',#125240);
#11362=VERTEX_POINT('',#125242);
#11363=VERTEX_POINT('',#125247);
#11364=VERTEX_POINT('',#125255);
#11365=VERTEX_POINT('',#125257);
#11366=VERTEX_POINT('',#125261);
#11367=VERTEX_POINT('',#125265);
#11368=VERTEX_POINT('',#125269);
#11369=VERTEX_POINT('',#125273);
#11370=VERTEX_POINT('',#125277);
#11371=VERTEX_POINT('',#125281);
#11372=VERTEX_POINT('',#125285);
#11373=VERTEX_POINT('',#125289);
#11374=VERTEX_POINT('',#125293);
#11375=VERTEX_POINT('',#125295);
#11376=VERTEX_POINT('',#125297);
#11377=VERTEX_POINT('',#125301);
#11378=VERTEX_POINT('',#125305);
#11379=VERTEX_POINT('',#125309);
#11380=VERTEX_POINT('',#125311);
#11381=VERTEX_POINT('',#125313);
#11382=VERTEX_POINT('',#125317);
#11383=VERTEX_POINT('',#125321);
#11384=VERTEX_POINT('',#125325);
#11385=VERTEX_POINT('',#125329);
#11386=VERTEX_POINT('',#125334);
#11387=VERTEX_POINT('',#125349);
#11388=VERTEX_POINT('',#125353);
#11389=VERTEX_POINT('',#125356);
#11390=VERTEX_POINT('',#125378);
#11391=VERTEX_POINT('',#125383);
#11392=VERTEX_POINT('',#125387);
#11393=VERTEX_POINT('',#125392);
#11394=VERTEX_POINT('',#125393);
#11395=VERTEX_POINT('',#125395);
#11396=VERTEX_POINT('',#125410);
#11397=VERTEX_POINT('',#125412);
#11398=VERTEX_POINT('',#125435);
#11399=VERTEX_POINT('',#125442);
#11400=VERTEX_POINT('',#125446);
#11401=VERTEX_POINT('',#125448);
#11402=VERTEX_POINT('',#125450);
#11403=VERTEX_POINT('',#125452);
#11404=VERTEX_POINT('',#125454);
#11405=VERTEX_POINT('',#125456);
#11406=VERTEX_POINT('',#125458);
#11407=VERTEX_POINT('',#125460);
#11408=VERTEX_POINT('',#125462);
#11409=VERTEX_POINT('',#125464);
#11410=VERTEX_POINT('',#125466);
#11411=VERTEX_POINT('',#125468);
#11412=VERTEX_POINT('',#125470);
#11413=VERTEX_POINT('',#125472);
#11414=VERTEX_POINT('',#125474);
#11415=VERTEX_POINT('',#125476);
#11416=VERTEX_POINT('',#125478);
#11417=VERTEX_POINT('',#125480);
#11418=VERTEX_POINT('',#125482);
#11419=VERTEX_POINT('',#125486);
#11420=VERTEX_POINT('',#125488);
#11421=VERTEX_POINT('',#125519);
#11422=VERTEX_POINT('',#125520);
#11423=VERTEX_POINT('',#125525);
#11424=VERTEX_POINT('',#125531);
#11425=VERTEX_POINT('',#125532);
#11426=VERTEX_POINT('',#125537);
#11427=VERTEX_POINT('',#125543);
#11428=VERTEX_POINT('',#125547);
#11429=VERTEX_POINT('',#125551);
#11430=VERTEX_POINT('',#125563);
#11431=VERTEX_POINT('',#125593);
#11432=VERTEX_POINT('',#125595);
#11433=VERTEX_POINT('',#125599);
#11434=VERTEX_POINT('',#125606);
#11435=VERTEX_POINT('',#125608);
#14930=EDGE_CURVE('',#11294,#11294,#5890,.T.);
#14931=EDGE_CURVE('',#11294,#11295,#6960,.T.);
#14932=EDGE_CURVE('',#11295,#11295,#5891,.T.);
#14933=EDGE_CURVE('',#11296,#11296,#5892,.T.);
#14934=EDGE_CURVE('',#11296,#11297,#6961,.T.);
#14935=EDGE_CURVE('',#11297,#11297,#5893,.T.);
#14936=EDGE_CURVE('',#11298,#11299,#6962,.T.);
#14937=EDGE_CURVE('',#11300,#11298,#107,.T.);
#14938=EDGE_CURVE('',#11301,#11300,#6963,.T.);
#14939=EDGE_CURVE('',#11299,#11301,#5894,.T.);
#14940=EDGE_CURVE('',#11302,#11301,#6964,.T.);
#14941=EDGE_CURVE('',#11303,#11302,#5895,.T.);
#14942=EDGE_CURVE('',#11299,#11303,#6965,.T.);
#14943=EDGE_CURVE('',#11304,#11305,#5896,.T.);
#14944=EDGE_CURVE('',#11306,#11304,#6966,.T.);
#14945=EDGE_CURVE('',#11307,#11306,#5897,.T.);
#14946=EDGE_CURVE('',#11305,#11307,#6967,.T.);
#14947=EDGE_CURVE('',#11308,#11309,#5898,.T.);
#14948=EDGE_CURVE('',#11307,#11308,#5899,.T.);
#14949=EDGE_CURVE('',#11309,#11306,#5900,.T.);
#14950=EDGE_CURVE('',#11310,#11311,#5901,.T.);
#14951=EDGE_CURVE('',#11308,#11310,#6968,.T.);
#14952=EDGE_CURVE('',#11311,#11309,#6969,.T.);
#14953=EDGE_CURVE('',#11312,#11313,#5902,.T.);
#14954=EDGE_CURVE('',#11310,#11312,#5903,.T.);
#14955=EDGE_CURVE('',#11313,#11311,#5904,.T.);
#14956=EDGE_CURVE('',#11314,#11315,#5905,.T.);
#14957=EDGE_CURVE('',#11312,#11314,#6970,.T.);
#14958=EDGE_CURVE('',#11315,#11313,#6971,.T.);
#14959=EDGE_CURVE('',#11316,#11317,#5906,.T.);
#14960=EDGE_CURVE('',#11314,#11316,#5907,.T.);
#14961=EDGE_CURVE('',#11317,#11315,#5908,.T.);
#14962=EDGE_CURVE('',#11318,#11319,#5909,.T.);
#14963=EDGE_CURVE('',#11316,#11318,#6972,.T.);
#14964=EDGE_CURVE('',#11319,#11317,#6973,.T.);
#14965=EDGE_CURVE('',#11320,#11321,#5910,.T.);
#14966=EDGE_CURVE('',#11318,#11320,#5911,.T.);
#14967=EDGE_CURVE('',#11321,#11319,#5912,.T.);
#14968=EDGE_CURVE('',#11322,#11321,#6974,.T.);
#14969=EDGE_CURVE('',#11323,#11322,#108,.T.);
#14970=EDGE_CURVE('',#11320,#11323,#6975,.T.);
#14971=EDGE_CURVE('',#11324,#11322,#6976,.T.);
#14972=EDGE_CURVE('',#11325,#11324,#109,.T.);
#14973=EDGE_CURVE('',#11323,#11325,#6977,.T.);
#14974=EDGE_CURVE('',#11325,#11326,#6978,.T.);
#14975=EDGE_CURVE('',#11327,#11324,#6979,.T.);
#14976=EDGE_CURVE('',#11326,#11327,#5913,.T.);
#14977=EDGE_CURVE('',#11328,#11329,#5914,.T.);
#14978=EDGE_CURVE('',#11326,#11328,#5915,.T.);
#14979=EDGE_CURVE('',#11329,#11327,#5916,.T.);
#14980=EDGE_CURVE('',#11330,#11329,#6980,.T.);
#14981=EDGE_CURVE('',#11331,#11330,#110,.T.);
#14982=EDGE_CURVE('',#11328,#11331,#6981,.T.);
#14983=EDGE_CURVE('',#11331,#11302,#6982,.T.);
#14984=EDGE_CURVE('',#11303,#11330,#6983,.T.);
#14985=EDGE_CURVE('',#11300,#11332,#6984,.T.);
#14986=EDGE_CURVE('',#11333,#11298,#6985,.T.);
#14987=EDGE_CURVE('',#11332,#11333,#5917,.T.);
#14988=EDGE_CURVE('',#11334,#11335,#5918,.T.);
#14989=EDGE_CURVE('',#11332,#11334,#5919,.T.);
#14990=EDGE_CURVE('',#11335,#11333,#5920,.T.);
#14991=EDGE_CURVE('',#11336,#11335,#6986,.T.);
#14992=EDGE_CURVE('',#11337,#11336,#111,.T.);
#14993=EDGE_CURVE('',#11334,#11337,#6987,.T.);
#14994=EDGE_CURVE('',#11337,#11338,#6988,.T.);
#14995=EDGE_CURVE('',#11339,#11336,#6989,.T.);
#14996=EDGE_CURVE('',#11338,#11339,#112,.T.);
#14997=EDGE_CURVE('',#11338,#11340,#6990,.T.);
#14998=EDGE_CURVE('',#11341,#11339,#6991,.T.);
#14999=EDGE_CURVE('',#11340,#11341,#5921,.T.);
#15000=EDGE_CURVE('',#11342,#11343,#5922,.T.);
#15001=EDGE_CURVE('',#11340,#11342,#5923,.T.);
#15002=EDGE_CURVE('',#11343,#11341,#5924,.T.);
#15003=EDGE_CURVE('',#11344,#11345,#5925,.T.);
#15004=EDGE_CURVE('',#11342,#11344,#6992,.T.);
#15005=EDGE_CURVE('',#11345,#11343,#6993,.T.);
#15006=EDGE_CURVE('',#11346,#11347,#5926,.T.);
#15007=EDGE_CURVE('',#11344,#11346,#5927,.T.);
#15008=EDGE_CURVE('',#11347,#11345,#5928,.T.);
#15009=EDGE_CURVE('',#11348,#11349,#5929,.T.);
#15010=EDGE_CURVE('',#11346,#11348,#6994,.T.);
#15011=EDGE_CURVE('',#11349,#11347,#6995,.T.);
#15012=EDGE_CURVE('',#11350,#11351,#5930,.T.);
#15013=EDGE_CURVE('',#11348,#11350,#5931,.T.);
#15014=EDGE_CURVE('',#11351,#11349,#5932,.T.);
#15015=EDGE_CURVE('',#11352,#11353,#5933,.T.);
#15016=EDGE_CURVE('',#11350,#11352,#6996,.T.);
#15017=EDGE_CURVE('',#11353,#11351,#6997,.T.);
#15018=EDGE_CURVE('',#11354,#11355,#5934,.T.);
#15019=EDGE_CURVE('',#11352,#11354,#5935,.T.);
#15020=EDGE_CURVE('',#11355,#11353,#5936,.T.);
#15021=EDGE_CURVE('',#11356,#11357,#5937,.T.);
#15022=EDGE_CURVE('',#11354,#11356,#6998,.T.);
#15023=EDGE_CURVE('',#11357,#11355,#6999,.T.);
#15024=EDGE_CURVE('',#11358,#11359,#5938,.T.);
#15025=EDGE_CURVE('',#11360,#11358,#7000,.T.);
#15026=EDGE_CURVE('',#11305,#11360,#5939,.T.);
#15027=EDGE_CURVE('',#11359,#11305,#7001,.T.);
#15028=EDGE_CURVE('',#11361,#11359,#7002,.T.);
#15029=EDGE_CURVE('',#11362,#11361,#5940,.T.);
#15030=EDGE_CURVE('',#11358,#11362,#7003,.T.);
#15031=EDGE_CURVE('',#11356,#11361,#7004,.T.);
#15032=EDGE_CURVE('',#11363,#11356,#5941,.T.);
#15033=EDGE_CURVE('',#11362,#11363,#7005,.T.);
#15034=EDGE_CURVE('',#11363,#11357,#5942,.T.);
#15035=EDGE_CURVE('',#11304,#11360,#5943,.T.);
#15036=EDGE_CURVE('',#11298,#11364,#7006,.T.);
#15037=EDGE_CURVE('',#11364,#11365,#7007,.T.);
#15038=EDGE_CURVE('',#11333,#11365,#7008,.T.);
#15039=EDGE_CURVE('',#11365,#11366,#5944,.T.);
#15040=EDGE_CURVE('',#11335,#11366,#7009,.T.);
#15041=EDGE_CURVE('',#11366,#11367,#7010,.T.);
#15042=EDGE_CURVE('',#11336,#11367,#7011,.T.);
#15043=EDGE_CURVE('',#11367,#11368,#7012,.T.);
#15044=EDGE_CURVE('',#11339,#11368,#7013,.T.);
#15045=EDGE_CURVE('',#11368,#11369,#7014,.T.);
#15046=EDGE_CURVE('',#11341,#11369,#7015,.T.);
#15047=EDGE_CURVE('',#11369,#11370,#5945,.T.);
#15048=EDGE_CURVE('',#11343,#11370,#7016,.T.);
#15049=EDGE_CURVE('',#11370,#11371,#7017,.T.);
#15050=EDGE_CURVE('',#11345,#11371,#7018,.T.);
#15051=EDGE_CURVE('',#11371,#11372,#5946,.T.);
#15052=EDGE_CURVE('',#11347,#11372,#7019,.T.);
#15053=EDGE_CURVE('',#11372,#11373,#7020,.T.);
#15054=EDGE_CURVE('',#11349,#11373,#7021,.T.);
#15055=EDGE_CURVE('',#11373,#11374,#5947,.T.);
#15056=EDGE_CURVE('',#11375,#11374,#7022,.T.);
#15057=EDGE_CURVE('',#11376,#11375,#5948,.T.);
#15058=EDGE_CURVE('',#11351,#11376,#7023,.T.);
#15059=EDGE_CURVE('',#11377,#11376,#7024,.T.);
#15060=EDGE_CURVE('',#11353,#11377,#7025,.T.);
#15061=EDGE_CURVE('',#11378,#11377,#5949,.T.);
#15062=EDGE_CURVE('',#11355,#11378,#7026,.T.);
#15063=EDGE_CURVE('',#11379,#11378,#7027,.T.);
#15064=EDGE_CURVE('',#11380,#11379,#7028,.T.);
#15065=EDGE_CURVE('',#11380,#11381,#7029,.T.);
#15066=EDGE_CURVE('',#11357,#11381,#7030,.T.);
#15067=EDGE_CURVE('',#11381,#11382,#5950,.T.);
#15068=EDGE_CURVE('',#11363,#11382,#7031,.T.);
#15069=EDGE_CURVE('',#11382,#11383,#7032,.T.);
#15070=EDGE_CURVE('',#11362,#11383,#7033,.T.);
#15071=EDGE_CURVE('',#11383,#11384,#7034,.T.);
#15072=EDGE_CURVE('',#11358,#11384,#7035,.T.);
#15073=EDGE_CURVE('',#11384,#11385,#7036,.T.);
#15074=EDGE_CURVE('',#11360,#11385,#7037,.T.);
#15075=EDGE_CURVE('',#11386,#11380,#1149,.T.);
#15076=EDGE_CURVE('',#11387,#11386,#7038,.T.);
#15077=EDGE_CURVE('',#11381,#11387,#5951,.T.);
#15078=EDGE_CURVE('',#11386,#11388,#5952,.T.);
#15079=EDGE_CURVE('',#11374,#11380,#5953,.T.);
#15080=EDGE_CURVE('',#11389,#11374,#1150,.T.);
#15081=EDGE_CURVE('',#11388,#11389,#1151,.T.);
#15082=EDGE_CURVE('',#11383,#11390,#5954,.T.);
#15083=EDGE_CURVE('',#11387,#11382,#5955,.T.);
#15084=EDGE_CURVE('',#11390,#11387,#7039,.T.);
#15085=EDGE_CURVE('',#11384,#11391,#5956,.T.);
#15086=EDGE_CURVE('',#11391,#11390,#7040,.T.);
#15087=EDGE_CURVE('',#11392,#11391,#7041,.T.);
#15088=EDGE_CURVE('',#11385,#11392,#5957,.T.);
#15089=EDGE_CURVE('',#11393,#11394,#5958,.T.);
#15090=EDGE_CURVE('',#11395,#11393,#1152,.T.);
#15091=EDGE_CURVE('',#11396,#11395,#5959,.T.);
#15092=EDGE_CURVE('',#11397,#11396,#1153,.T.);
#15093=EDGE_CURVE('',#11394,#11397,#1154,.T.);
#15094=EDGE_CURVE('',#11395,#11392,#7042,.T.);
#15095=EDGE_CURVE('',#11398,#11393,#7043,.T.);
#15096=EDGE_CURVE('',#11392,#11398,#5960,.T.);
#15097=EDGE_CURVE('',#11385,#11398,#5961,.T.);
#15098=EDGE_CURVE('',#11373,#11389,#5962,.T.);
#15099=EDGE_CURVE('',#11372,#11399,#5963,.T.);
#15100=EDGE_CURVE('',#11388,#11399,#7044,.T.);
#15101=EDGE_CURVE('',#11399,#11400,#5964,.T.);
#15102=EDGE_CURVE('',#11400,#11401,#7045,.T.);
#15103=EDGE_CURVE('',#11401,#11402,#5965,.T.);
#15104=EDGE_CURVE('',#11402,#11403,#7046,.T.);
#15105=EDGE_CURVE('',#11403,#11404,#7047,.T.);
#15106=EDGE_CURVE('',#11404,#11405,#7048,.T.);
#15107=EDGE_CURVE('',#11405,#11406,#5966,.T.);
#15108=EDGE_CURVE('',#11406,#11407,#7049,.T.);
#15109=EDGE_CURVE('',#11407,#11408,#7050,.T.);
#15110=EDGE_CURVE('',#11408,#11409,#7051,.T.);
#15111=EDGE_CURVE('',#11409,#11410,#7052,.T.);
#15112=EDGE_CURVE('',#11410,#11411,#7053,.T.);
#15113=EDGE_CURVE('',#11411,#11412,#5967,.T.);
#15114=EDGE_CURVE('',#11412,#11413,#7054,.T.);
#15115=EDGE_CURVE('',#11413,#11414,#7055,.T.);
#15116=EDGE_CURVE('',#11414,#11415,#7056,.T.);
#15117=EDGE_CURVE('',#11415,#11416,#5968,.T.);
#15118=EDGE_CURVE('',#11416,#11417,#7057,.T.);
#15119=EDGE_CURVE('',#11417,#11418,#5969,.T.);
#15120=EDGE_CURVE('',#11418,#11396,#7058,.T.);
#15121=EDGE_CURVE('',#11419,#11418,#5970,.T.);
#15122=EDGE_CURVE('',#11420,#11419,#7059,.T.);
#15123=EDGE_CURVE('',#11420,#11397,#5971,.T.);
#15124=EDGE_CURVE('',#11394,#11420,#5972,.T.);
#15125=EDGE_CURVE('',#11403,#11368,#113,.T.);
#15126=EDGE_CURVE('',#11369,#11402,#5973,.T.);
#15127=EDGE_CURVE('',#11370,#11401,#5974,.T.);
#15128=EDGE_CURVE('',#11371,#11400,#5975,.T.);
#15129=EDGE_CURVE('',#11404,#11367,#114,.T.);
#15130=EDGE_CURVE('',#11407,#11364,#115,.T.);
#15131=EDGE_CURVE('',#11365,#11406,#5976,.T.);
#15132=EDGE_CURVE('',#11366,#11405,#5977,.T.);
#15133=EDGE_CURVE('',#11421,#11422,#7060,.T.);
#15134=EDGE_CURVE('',#11410,#11421,#116,.T.);
#15135=EDGE_CURVE('',#11422,#11409,#5978,.T.);
#15136=EDGE_CURVE('',#11423,#11408,#5979,.T.);
#15137=EDGE_CURVE('',#11422,#11423,#7061,.T.);
#15138=EDGE_CURVE('',#11423,#11364,#7062,.T.);
#15139=EDGE_CURVE('',#11424,#11425,#7063,.T.);
#15140=EDGE_CURVE('',#11413,#11424,#117,.T.);
#15141=EDGE_CURVE('',#11425,#11412,#5980,.T.);
#15142=EDGE_CURVE('',#11426,#11411,#5981,.T.);
#15143=EDGE_CURVE('',#11425,#11426,#5982,.T.);
#15144=EDGE_CURVE('',#11426,#11421,#7064,.T.);
#15145=EDGE_CURVE('',#11427,#11424,#7065,.T.);
#15146=EDGE_CURVE('',#11414,#11427,#118,.T.);
#15147=EDGE_CURVE('',#11428,#11417,#5983,.T.);
#15148=EDGE_CURVE('',#11419,#11428,#5984,.T.);
#15149=EDGE_CURVE('',#11429,#11416,#5985,.T.);
#15150=EDGE_CURVE('',#11428,#11429,#7066,.T.);
#15151=EDGE_CURVE('',#11430,#11415,#5986,.T.);
#15152=EDGE_CURVE('',#11429,#11430,#5987,.T.);
#15153=EDGE_CURVE('',#11430,#11427,#7067,.T.);
#15154=EDGE_CURVE('',#11299,#11423,#7068,.T.);
#15155=EDGE_CURVE('',#11303,#11422,#7069,.T.);
#15156=EDGE_CURVE('',#11330,#11421,#7070,.T.);
#15157=EDGE_CURVE('',#11329,#11426,#7071,.T.);
#15158=EDGE_CURVE('',#11327,#11425,#7072,.T.);
#15159=EDGE_CURVE('',#11324,#11424,#7073,.T.);
#15160=EDGE_CURVE('',#11322,#11427,#7074,.T.);
#15161=EDGE_CURVE('',#11321,#11430,#7075,.T.);
#15162=EDGE_CURVE('',#11319,#11429,#7076,.T.);
#15163=EDGE_CURVE('',#11317,#11428,#7077,.T.);
#15164=EDGE_CURVE('',#11315,#11419,#7078,.T.);
#15165=EDGE_CURVE('',#11313,#11420,#7079,.T.);
#15166=EDGE_CURVE('',#11311,#11431,#7080,.T.);
#15167=EDGE_CURVE('',#11432,#11431,#5988,.T.);
#15168=EDGE_CURVE('',#11394,#11432,#7081,.T.);
#15169=EDGE_CURVE('',#11433,#11432,#5989,.T.);
#15170=EDGE_CURVE('',#11433,#11393,#7082,.T.);
#15171=EDGE_CURVE('',#11375,#11379,#5990,.T.);
#15172=EDGE_CURVE('',#11431,#11434,#7083,.T.);
#15173=EDGE_CURVE('',#11434,#11435,#5991,.T.);
#15174=EDGE_CURVE('',#11435,#11433,#7084,.T.);
#15175=EDGE_CURVE('',#11309,#11434,#7085,.T.);
#15176=EDGE_CURVE('',#11306,#11435,#7086,.T.);
#15177=EDGE_CURVE('',#11304,#11398,#7087,.T.);
#21137=ORIENTED_EDGE('',*,*,#14930,.T.);
#21138=ORIENTED_EDGE('',*,*,#14931,.T.);
#21139=ORIENTED_EDGE('',*,*,#14932,.T.);
#21140=ORIENTED_EDGE('',*,*,#14931,.F.);
#21141=ORIENTED_EDGE('',*,*,#14932,.F.);
#21142=ORIENTED_EDGE('',*,*,#14933,.F.);
#21143=ORIENTED_EDGE('',*,*,#14934,.T.);
#21144=ORIENTED_EDGE('',*,*,#14935,.T.);
#21145=ORIENTED_EDGE('',*,*,#14934,.F.);
#21146=ORIENTED_EDGE('',*,*,#14933,.T.);
#21147=ORIENTED_EDGE('',*,*,#14936,.F.);
#21148=ORIENTED_EDGE('',*,*,#14937,.F.);
#21149=ORIENTED_EDGE('',*,*,#14938,.F.);
#21150=ORIENTED_EDGE('',*,*,#14939,.F.);
#21151=ORIENTED_EDGE('',*,*,#14939,.T.);
#21152=ORIENTED_EDGE('',*,*,#14940,.F.);
#21153=ORIENTED_EDGE('',*,*,#14941,.F.);
#21154=ORIENTED_EDGE('',*,*,#14942,.F.);
#21155=ORIENTED_EDGE('',*,*,#14943,.F.);
#21156=ORIENTED_EDGE('',*,*,#14944,.F.);
#21157=ORIENTED_EDGE('',*,*,#14945,.F.);
#21158=ORIENTED_EDGE('',*,*,#14946,.F.);
#21159=ORIENTED_EDGE('',*,*,#14947,.F.);
#21160=ORIENTED_EDGE('',*,*,#14948,.F.);
#21161=ORIENTED_EDGE('',*,*,#14945,.T.);
#21162=ORIENTED_EDGE('',*,*,#14949,.F.);
#21163=ORIENTED_EDGE('',*,*,#14950,.F.);
#21164=ORIENTED_EDGE('',*,*,#14951,.F.);
#21165=ORIENTED_EDGE('',*,*,#14947,.T.);
#21166=ORIENTED_EDGE('',*,*,#14952,.F.);
#21167=ORIENTED_EDGE('',*,*,#14953,.F.);
#21168=ORIENTED_EDGE('',*,*,#14954,.F.);
#21169=ORIENTED_EDGE('',*,*,#14950,.T.);
#21170=ORIENTED_EDGE('',*,*,#14955,.F.);
#21171=ORIENTED_EDGE('',*,*,#14956,.F.);
#21172=ORIENTED_EDGE('',*,*,#14957,.F.);
#21173=ORIENTED_EDGE('',*,*,#14953,.T.);
#21174=ORIENTED_EDGE('',*,*,#14958,.F.);
#21175=ORIENTED_EDGE('',*,*,#14959,.F.);
#21176=ORIENTED_EDGE('',*,*,#14960,.F.);
#21177=ORIENTED_EDGE('',*,*,#14956,.T.);
#21178=ORIENTED_EDGE('',*,*,#14961,.F.);
#21179=ORIENTED_EDGE('',*,*,#14962,.F.);
#21180=ORIENTED_EDGE('',*,*,#14963,.F.);
#21181=ORIENTED_EDGE('',*,*,#14959,.T.);
#21182=ORIENTED_EDGE('',*,*,#14964,.F.);
#21183=ORIENTED_EDGE('',*,*,#14965,.F.);
#21184=ORIENTED_EDGE('',*,*,#14966,.F.);
#21185=ORIENTED_EDGE('',*,*,#14962,.T.);
#21186=ORIENTED_EDGE('',*,*,#14967,.F.);
#21187=ORIENTED_EDGE('',*,*,#14968,.F.);
#21188=ORIENTED_EDGE('',*,*,#14969,.F.);
#21189=ORIENTED_EDGE('',*,*,#14970,.F.);
#21190=ORIENTED_EDGE('',*,*,#14965,.T.);
#21191=ORIENTED_EDGE('',*,*,#14971,.F.);
#21192=ORIENTED_EDGE('',*,*,#14972,.F.);
#21193=ORIENTED_EDGE('',*,*,#14973,.F.);
#21194=ORIENTED_EDGE('',*,*,#14969,.T.);
#21195=ORIENTED_EDGE('',*,*,#14974,.F.);
#21196=ORIENTED_EDGE('',*,*,#14972,.T.);
#21197=ORIENTED_EDGE('',*,*,#14975,.F.);
#21198=ORIENTED_EDGE('',*,*,#14976,.F.);
#21199=ORIENTED_EDGE('',*,*,#14977,.F.);
#21200=ORIENTED_EDGE('',*,*,#14978,.F.);
#21201=ORIENTED_EDGE('',*,*,#14976,.T.);
#21202=ORIENTED_EDGE('',*,*,#14979,.F.);
#21203=ORIENTED_EDGE('',*,*,#14980,.F.);
#21204=ORIENTED_EDGE('',*,*,#14981,.F.);
#21205=ORIENTED_EDGE('',*,*,#14982,.F.);
#21206=ORIENTED_EDGE('',*,*,#14977,.T.);
#21207=ORIENTED_EDGE('',*,*,#14941,.T.);
#21208=ORIENTED_EDGE('',*,*,#14983,.F.);
#21209=ORIENTED_EDGE('',*,*,#14981,.T.);
#21210=ORIENTED_EDGE('',*,*,#14984,.F.);
#21211=ORIENTED_EDGE('',*,*,#14985,.F.);
#21212=ORIENTED_EDGE('',*,*,#14937,.T.);
#21213=ORIENTED_EDGE('',*,*,#14986,.F.);
#21214=ORIENTED_EDGE('',*,*,#14987,.F.);
#21215=ORIENTED_EDGE('',*,*,#14988,.F.);
#21216=ORIENTED_EDGE('',*,*,#14989,.F.);
#21217=ORIENTED_EDGE('',*,*,#14987,.T.);
#21218=ORIENTED_EDGE('',*,*,#14990,.F.);
#21219=ORIENTED_EDGE('',*,*,#14991,.F.);
#21220=ORIENTED_EDGE('',*,*,#14992,.F.);
#21221=ORIENTED_EDGE('',*,*,#14993,.F.);
#21222=ORIENTED_EDGE('',*,*,#14988,.T.);
#21223=ORIENTED_EDGE('',*,*,#14994,.F.);
#21224=ORIENTED_EDGE('',*,*,#14992,.T.);
#21225=ORIENTED_EDGE('',*,*,#14995,.F.);
#21226=ORIENTED_EDGE('',*,*,#14996,.F.);
#21227=ORIENTED_EDGE('',*,*,#14997,.F.);
#21228=ORIENTED_EDGE('',*,*,#14996,.T.);
#21229=ORIENTED_EDGE('',*,*,#14998,.F.);
#21230=ORIENTED_EDGE('',*,*,#14999,.F.);
#21231=ORIENTED_EDGE('',*,*,#15000,.F.);
#21232=ORIENTED_EDGE('',*,*,#15001,.F.);
#21233=ORIENTED_EDGE('',*,*,#14999,.T.);
#21234=ORIENTED_EDGE('',*,*,#15002,.F.);
#21235=ORIENTED_EDGE('',*,*,#15003,.F.);
#21236=ORIENTED_EDGE('',*,*,#15004,.F.);
#21237=ORIENTED_EDGE('',*,*,#15000,.T.);
#21238=ORIENTED_EDGE('',*,*,#15005,.F.);
#21239=ORIENTED_EDGE('',*,*,#15006,.F.);
#21240=ORIENTED_EDGE('',*,*,#15007,.F.);
#21241=ORIENTED_EDGE('',*,*,#15003,.T.);
#21242=ORIENTED_EDGE('',*,*,#15008,.F.);
#21243=ORIENTED_EDGE('',*,*,#15009,.F.);
#21244=ORIENTED_EDGE('',*,*,#15010,.F.);
#21245=ORIENTED_EDGE('',*,*,#15006,.T.);
#21246=ORIENTED_EDGE('',*,*,#15011,.F.);
#21247=ORIENTED_EDGE('',*,*,#15012,.F.);
#21248=ORIENTED_EDGE('',*,*,#15013,.F.);
#21249=ORIENTED_EDGE('',*,*,#15009,.T.);
#21250=ORIENTED_EDGE('',*,*,#15014,.F.);
#21251=ORIENTED_EDGE('',*,*,#15015,.F.);
#21252=ORIENTED_EDGE('',*,*,#15016,.F.);
#21253=ORIENTED_EDGE('',*,*,#15012,.T.);
#21254=ORIENTED_EDGE('',*,*,#15017,.F.);
#21255=ORIENTED_EDGE('',*,*,#15018,.F.);
#21256=ORIENTED_EDGE('',*,*,#15019,.F.);
#21257=ORIENTED_EDGE('',*,*,#15015,.T.);
#21258=ORIENTED_EDGE('',*,*,#15020,.F.);
#21259=ORIENTED_EDGE('',*,*,#15021,.F.);
#21260=ORIENTED_EDGE('',*,*,#15022,.F.);
#21261=ORIENTED_EDGE('',*,*,#15018,.T.);
#21262=ORIENTED_EDGE('',*,*,#15023,.F.);
#21263=ORIENTED_EDGE('',*,*,#15024,.F.);
#21264=ORIENTED_EDGE('',*,*,#15025,.F.);
#21265=ORIENTED_EDGE('',*,*,#15026,.F.);
#21266=ORIENTED_EDGE('',*,*,#15027,.F.);
#21267=ORIENTED_EDGE('',*,*,#15024,.T.);
#21268=ORIENTED_EDGE('',*,*,#15028,.F.);
#21269=ORIENTED_EDGE('',*,*,#15029,.F.);
#21270=ORIENTED_EDGE('',*,*,#15030,.F.);
#21271=ORIENTED_EDGE('',*,*,#15029,.T.);
#21272=ORIENTED_EDGE('',*,*,#15031,.F.);
#21273=ORIENTED_EDGE('',*,*,#15032,.F.);
#21274=ORIENTED_EDGE('',*,*,#15033,.F.);
#21275=ORIENTED_EDGE('',*,*,#15032,.T.);
#21276=ORIENTED_EDGE('',*,*,#15021,.T.);
#21277=ORIENTED_EDGE('',*,*,#15034,.F.);
#21278=ORIENTED_EDGE('',*,*,#14943,.T.);
#21279=ORIENTED_EDGE('',*,*,#15026,.T.);
#21280=ORIENTED_EDGE('',*,*,#15035,.F.);
#21281=ORIENTED_EDGE('',*,*,#14986,.T.);
#21282=ORIENTED_EDGE('',*,*,#15036,.T.);
#21283=ORIENTED_EDGE('',*,*,#15037,.T.);
#21284=ORIENTED_EDGE('',*,*,#15038,.F.);
#21285=ORIENTED_EDGE('',*,*,#14990,.T.);
#21286=ORIENTED_EDGE('',*,*,#15038,.T.);
#21287=ORIENTED_EDGE('',*,*,#15039,.T.);
#21288=ORIENTED_EDGE('',*,*,#15040,.F.);
#21289=ORIENTED_EDGE('',*,*,#14991,.T.);
#21290=ORIENTED_EDGE('',*,*,#15040,.T.);
#21291=ORIENTED_EDGE('',*,*,#15041,.T.);
#21292=ORIENTED_EDGE('',*,*,#15042,.F.);
#21293=ORIENTED_EDGE('',*,*,#14995,.T.);
#21294=ORIENTED_EDGE('',*,*,#15042,.T.);
#21295=ORIENTED_EDGE('',*,*,#15043,.T.);
#21296=ORIENTED_EDGE('',*,*,#15044,.F.);
#21297=ORIENTED_EDGE('',*,*,#14998,.T.);
#21298=ORIENTED_EDGE('',*,*,#15044,.T.);
#21299=ORIENTED_EDGE('',*,*,#15045,.T.);
#21300=ORIENTED_EDGE('',*,*,#15046,.F.);
#21301=ORIENTED_EDGE('',*,*,#15002,.T.);
#21302=ORIENTED_EDGE('',*,*,#15046,.T.);
#21303=ORIENTED_EDGE('',*,*,#15047,.T.);
#21304=ORIENTED_EDGE('',*,*,#15048,.F.);
#21305=ORIENTED_EDGE('',*,*,#15005,.T.);
#21306=ORIENTED_EDGE('',*,*,#15048,.T.);
#21307=ORIENTED_EDGE('',*,*,#15049,.T.);
#21308=ORIENTED_EDGE('',*,*,#15050,.F.);
#21309=ORIENTED_EDGE('',*,*,#14935,.F.);
#21310=ORIENTED_EDGE('',*,*,#15008,.T.);
#21311=ORIENTED_EDGE('',*,*,#15050,.T.);
#21312=ORIENTED_EDGE('',*,*,#15051,.T.);
#21313=ORIENTED_EDGE('',*,*,#15052,.F.);
#21314=ORIENTED_EDGE('',*,*,#15011,.T.);
#21315=ORIENTED_EDGE('',*,*,#15052,.T.);
#21316=ORIENTED_EDGE('',*,*,#15053,.T.);
#21317=ORIENTED_EDGE('',*,*,#15054,.F.);
#21318=ORIENTED_EDGE('',*,*,#15014,.T.);
#21319=ORIENTED_EDGE('',*,*,#15054,.T.);
#21320=ORIENTED_EDGE('',*,*,#15055,.T.);
#21321=ORIENTED_EDGE('',*,*,#15056,.F.);
#21322=ORIENTED_EDGE('',*,*,#15057,.F.);
#21323=ORIENTED_EDGE('',*,*,#15058,.F.);
#21324=ORIENTED_EDGE('',*,*,#15017,.T.);
#21325=ORIENTED_EDGE('',*,*,#15058,.T.);
#21326=ORIENTED_EDGE('',*,*,#15059,.F.);
#21327=ORIENTED_EDGE('',*,*,#15060,.F.);
#21328=ORIENTED_EDGE('',*,*,#15020,.T.);
#21329=ORIENTED_EDGE('',*,*,#15060,.T.);
#21330=ORIENTED_EDGE('',*,*,#15061,.F.);
#21331=ORIENTED_EDGE('',*,*,#15062,.F.);
#21332=ORIENTED_EDGE('',*,*,#15023,.T.);
#21333=ORIENTED_EDGE('',*,*,#15062,.T.);
#21334=ORIENTED_EDGE('',*,*,#15063,.F.);
#21335=ORIENTED_EDGE('',*,*,#15064,.F.);
#21336=ORIENTED_EDGE('',*,*,#15065,.T.);
#21337=ORIENTED_EDGE('',*,*,#15066,.F.);
#21338=ORIENTED_EDGE('',*,*,#15034,.T.);
#21339=ORIENTED_EDGE('',*,*,#15066,.T.);
#21340=ORIENTED_EDGE('',*,*,#15067,.T.);
#21341=ORIENTED_EDGE('',*,*,#15068,.F.);
#21342=ORIENTED_EDGE('',*,*,#15033,.T.);
#21343=ORIENTED_EDGE('',*,*,#15068,.T.);
#21344=ORIENTED_EDGE('',*,*,#15069,.T.);
#21345=ORIENTED_EDGE('',*,*,#15070,.F.);
#21346=ORIENTED_EDGE('',*,*,#15030,.T.);
#21347=ORIENTED_EDGE('',*,*,#15070,.T.);
#21348=ORIENTED_EDGE('',*,*,#15071,.T.);
#21349=ORIENTED_EDGE('',*,*,#15072,.F.);
#21350=ORIENTED_EDGE('',*,*,#15025,.T.);
#21351=ORIENTED_EDGE('',*,*,#15072,.T.);
#21352=ORIENTED_EDGE('',*,*,#15073,.T.);
#21353=ORIENTED_EDGE('',*,*,#15074,.F.);
#21354=ORIENTED_EDGE('',*,*,#14946,.T.);
#21355=ORIENTED_EDGE('',*,*,#14948,.T.);
#21356=ORIENTED_EDGE('',*,*,#14951,.T.);
#21357=ORIENTED_EDGE('',*,*,#14954,.T.);
#21358=ORIENTED_EDGE('',*,*,#14957,.T.);
#21359=ORIENTED_EDGE('',*,*,#14960,.T.);
#21360=ORIENTED_EDGE('',*,*,#14963,.T.);
#21361=ORIENTED_EDGE('',*,*,#14966,.T.);
#21362=ORIENTED_EDGE('',*,*,#14970,.T.);
#21363=ORIENTED_EDGE('',*,*,#14973,.T.);
#21364=ORIENTED_EDGE('',*,*,#14974,.T.);
#21365=ORIENTED_EDGE('',*,*,#14978,.T.);
#21366=ORIENTED_EDGE('',*,*,#14982,.T.);
#21367=ORIENTED_EDGE('',*,*,#14983,.T.);
#21368=ORIENTED_EDGE('',*,*,#14940,.T.);
#21369=ORIENTED_EDGE('',*,*,#14938,.T.);
#21370=ORIENTED_EDGE('',*,*,#14985,.T.);
#21371=ORIENTED_EDGE('',*,*,#14989,.T.);
#21372=ORIENTED_EDGE('',*,*,#14993,.T.);
#21373=ORIENTED_EDGE('',*,*,#14994,.T.);
#21374=ORIENTED_EDGE('',*,*,#14997,.T.);
#21375=ORIENTED_EDGE('',*,*,#15001,.T.);
#21376=ORIENTED_EDGE('',*,*,#15004,.T.);
#21377=ORIENTED_EDGE('',*,*,#15007,.T.);
#21378=ORIENTED_EDGE('',*,*,#15010,.T.);
#21379=ORIENTED_EDGE('',*,*,#15013,.T.);
#21380=ORIENTED_EDGE('',*,*,#15016,.T.);
#21381=ORIENTED_EDGE('',*,*,#15019,.T.);
#21382=ORIENTED_EDGE('',*,*,#15022,.T.);
#21383=ORIENTED_EDGE('',*,*,#15031,.T.);
#21384=ORIENTED_EDGE('',*,*,#15028,.T.);
#21385=ORIENTED_EDGE('',*,*,#15027,.T.);
#21386=ORIENTED_EDGE('',*,*,#15065,.F.);
#21387=ORIENTED_EDGE('',*,*,#15075,.F.);
#21388=ORIENTED_EDGE('',*,*,#15076,.F.);
#21389=ORIENTED_EDGE('',*,*,#15077,.F.);
#21390=ORIENTED_EDGE('',*,*,#15078,.F.);
#21391=ORIENTED_EDGE('',*,*,#15075,.T.);
#21392=ORIENTED_EDGE('',*,*,#15079,.F.);
#21393=ORIENTED_EDGE('',*,*,#15080,.F.);
#21394=ORIENTED_EDGE('',*,*,#15081,.F.);
#21395=ORIENTED_EDGE('',*,*,#15082,.F.);
#21396=ORIENTED_EDGE('',*,*,#15069,.F.);
#21397=ORIENTED_EDGE('',*,*,#15083,.F.);
#21398=ORIENTED_EDGE('',*,*,#15084,.F.);
#21399=ORIENTED_EDGE('',*,*,#15085,.F.);
#21400=ORIENTED_EDGE('',*,*,#15071,.F.);
#21401=ORIENTED_EDGE('',*,*,#15082,.T.);
#21402=ORIENTED_EDGE('',*,*,#15086,.F.);
#21403=ORIENTED_EDGE('',*,*,#15085,.T.);
#21404=ORIENTED_EDGE('',*,*,#15087,.F.);
#21405=ORIENTED_EDGE('',*,*,#15088,.F.);
#21406=ORIENTED_EDGE('',*,*,#15073,.F.);
#21407=ORIENTED_EDGE('',*,*,#15083,.T.);
#21408=ORIENTED_EDGE('',*,*,#15067,.F.);
#21409=ORIENTED_EDGE('',*,*,#15077,.T.);
#21410=ORIENTED_EDGE('',*,*,#15089,.F.);
#21411=ORIENTED_EDGE('',*,*,#15090,.F.);
#21412=ORIENTED_EDGE('',*,*,#15091,.F.);
#21413=ORIENTED_EDGE('',*,*,#15092,.F.);
#21414=ORIENTED_EDGE('',*,*,#15093,.F.);
#21415=ORIENTED_EDGE('',*,*,#15094,.F.);
#21416=ORIENTED_EDGE('',*,*,#15090,.T.);
#21417=ORIENTED_EDGE('',*,*,#15095,.F.);
#21418=ORIENTED_EDGE('',*,*,#15096,.F.);
#21419=ORIENTED_EDGE('',*,*,#15096,.T.);
#21420=ORIENTED_EDGE('',*,*,#15097,.F.);
#21421=ORIENTED_EDGE('',*,*,#15088,.T.);
#21422=ORIENTED_EDGE('',*,*,#15081,.T.);
#21423=ORIENTED_EDGE('',*,*,#15098,.F.);
#21424=ORIENTED_EDGE('',*,*,#15053,.F.);
#21425=ORIENTED_EDGE('',*,*,#15099,.T.);
#21426=ORIENTED_EDGE('',*,*,#15100,.F.);
#21427=ORIENTED_EDGE('',*,*,#15078,.T.);
#21428=ORIENTED_EDGE('',*,*,#15100,.T.);
#21429=ORIENTED_EDGE('',*,*,#15101,.T.);
#21430=ORIENTED_EDGE('',*,*,#15102,.T.);
#21431=ORIENTED_EDGE('',*,*,#15103,.T.);
#21432=ORIENTED_EDGE('',*,*,#15104,.T.);
#21433=ORIENTED_EDGE('',*,*,#15105,.T.);
#21434=ORIENTED_EDGE('',*,*,#15106,.T.);
#21435=ORIENTED_EDGE('',*,*,#15107,.T.);
#21436=ORIENTED_EDGE('',*,*,#15108,.T.);
#21437=ORIENTED_EDGE('',*,*,#15109,.T.);
#21438=ORIENTED_EDGE('',*,*,#15110,.T.);
#21439=ORIENTED_EDGE('',*,*,#15111,.T.);
#21440=ORIENTED_EDGE('',*,*,#15112,.T.);
#21441=ORIENTED_EDGE('',*,*,#15113,.T.);
#21442=ORIENTED_EDGE('',*,*,#15114,.T.);
#21443=ORIENTED_EDGE('',*,*,#15115,.T.);
#21444=ORIENTED_EDGE('',*,*,#15116,.T.);
#21445=ORIENTED_EDGE('',*,*,#15117,.T.);
#21446=ORIENTED_EDGE('',*,*,#15118,.T.);
#21447=ORIENTED_EDGE('',*,*,#15119,.T.);
#21448=ORIENTED_EDGE('',*,*,#15120,.T.);
#21449=ORIENTED_EDGE('',*,*,#15091,.T.);
#21450=ORIENTED_EDGE('',*,*,#15094,.T.);
#21451=ORIENTED_EDGE('',*,*,#15087,.T.);
#21452=ORIENTED_EDGE('',*,*,#15086,.T.);
#21453=ORIENTED_EDGE('',*,*,#15084,.T.);
#21454=ORIENTED_EDGE('',*,*,#15076,.T.);
#21455=ORIENTED_EDGE('',*,*,#15092,.T.);
#21456=ORIENTED_EDGE('',*,*,#15120,.F.);
#21457=ORIENTED_EDGE('',*,*,#15121,.F.);
#21458=ORIENTED_EDGE('',*,*,#15122,.F.);
#21459=ORIENTED_EDGE('',*,*,#15123,.T.);
#21460=ORIENTED_EDGE('',*,*,#15093,.T.);
#21461=ORIENTED_EDGE('',*,*,#15123,.F.);
#21462=ORIENTED_EDGE('',*,*,#15124,.F.);
#21463=ORIENTED_EDGE('',*,*,#15045,.F.);
#21464=ORIENTED_EDGE('',*,*,#15125,.F.);
#21465=ORIENTED_EDGE('',*,*,#15104,.F.);
#21466=ORIENTED_EDGE('',*,*,#15126,.F.);
#21467=ORIENTED_EDGE('',*,*,#15127,.F.);
#21468=ORIENTED_EDGE('',*,*,#15047,.F.);
#21469=ORIENTED_EDGE('',*,*,#15126,.T.);
#21470=ORIENTED_EDGE('',*,*,#15103,.F.);
#21471=ORIENTED_EDGE('',*,*,#15128,.F.);
#21472=ORIENTED_EDGE('',*,*,#15049,.F.);
#21473=ORIENTED_EDGE('',*,*,#15127,.T.);
#21474=ORIENTED_EDGE('',*,*,#15102,.F.);
#21475=ORIENTED_EDGE('',*,*,#15099,.F.);
#21476=ORIENTED_EDGE('',*,*,#15051,.F.);
#21477=ORIENTED_EDGE('',*,*,#15128,.T.);
#21478=ORIENTED_EDGE('',*,*,#15101,.F.);
#21479=ORIENTED_EDGE('',*,*,#15080,.T.);
#21480=ORIENTED_EDGE('',*,*,#15055,.F.);
#21481=ORIENTED_EDGE('',*,*,#15098,.T.);
#21482=ORIENTED_EDGE('',*,*,#15043,.F.);
#21483=ORIENTED_EDGE('',*,*,#15129,.F.);
#21484=ORIENTED_EDGE('',*,*,#15105,.F.);
#21485=ORIENTED_EDGE('',*,*,#15125,.T.);
#21486=ORIENTED_EDGE('',*,*,#15037,.F.);
#21487=ORIENTED_EDGE('',*,*,#15130,.F.);
#21488=ORIENTED_EDGE('',*,*,#15108,.F.);
#21489=ORIENTED_EDGE('',*,*,#15131,.F.);
#21490=ORIENTED_EDGE('',*,*,#15132,.F.);
#21491=ORIENTED_EDGE('',*,*,#15039,.F.);
#21492=ORIENTED_EDGE('',*,*,#15131,.T.);
#21493=ORIENTED_EDGE('',*,*,#15107,.F.);
#21494=ORIENTED_EDGE('',*,*,#15106,.F.);
#21495=ORIENTED_EDGE('',*,*,#15129,.T.);
#21496=ORIENTED_EDGE('',*,*,#15041,.F.);
#21497=ORIENTED_EDGE('',*,*,#15132,.T.);
#21498=ORIENTED_EDGE('',*,*,#15133,.F.);
#21499=ORIENTED_EDGE('',*,*,#15134,.F.);
#21500=ORIENTED_EDGE('',*,*,#15111,.F.);
#21501=ORIENTED_EDGE('',*,*,#15135,.F.);
#21502=ORIENTED_EDGE('',*,*,#15136,.F.);
#21503=ORIENTED_EDGE('',*,*,#15137,.F.);
#21504=ORIENTED_EDGE('',*,*,#15135,.T.);
#21505=ORIENTED_EDGE('',*,*,#15110,.F.);
#21506=ORIENTED_EDGE('',*,*,#15109,.F.);
#21507=ORIENTED_EDGE('',*,*,#15130,.T.);
#21508=ORIENTED_EDGE('',*,*,#15138,.F.);
#21509=ORIENTED_EDGE('',*,*,#15136,.T.);
#21510=ORIENTED_EDGE('',*,*,#15139,.F.);
#21511=ORIENTED_EDGE('',*,*,#15140,.F.);
#21512=ORIENTED_EDGE('',*,*,#15114,.F.);
#21513=ORIENTED_EDGE('',*,*,#15141,.F.);
#21514=ORIENTED_EDGE('',*,*,#15142,.F.);
#21515=ORIENTED_EDGE('',*,*,#15143,.F.);
#21516=ORIENTED_EDGE('',*,*,#15141,.T.);
#21517=ORIENTED_EDGE('',*,*,#15113,.F.);
#21518=ORIENTED_EDGE('',*,*,#15112,.F.);
#21519=ORIENTED_EDGE('',*,*,#15134,.T.);
#21520=ORIENTED_EDGE('',*,*,#15144,.F.);
#21521=ORIENTED_EDGE('',*,*,#15142,.T.);
#21522=ORIENTED_EDGE('',*,*,#15145,.F.);
#21523=ORIENTED_EDGE('',*,*,#15146,.F.);
#21524=ORIENTED_EDGE('',*,*,#15115,.F.);
#21525=ORIENTED_EDGE('',*,*,#15140,.T.);
#21526=ORIENTED_EDGE('',*,*,#15147,.F.);
#21527=ORIENTED_EDGE('',*,*,#15148,.F.);
#21528=ORIENTED_EDGE('',*,*,#15121,.T.);
#21529=ORIENTED_EDGE('',*,*,#15119,.F.);
#21530=ORIENTED_EDGE('',*,*,#15149,.F.);
#21531=ORIENTED_EDGE('',*,*,#15150,.F.);
#21532=ORIENTED_EDGE('',*,*,#15147,.T.);
#21533=ORIENTED_EDGE('',*,*,#15118,.F.);
#21534=ORIENTED_EDGE('',*,*,#15151,.F.);
#21535=ORIENTED_EDGE('',*,*,#15152,.F.);
#21536=ORIENTED_EDGE('',*,*,#15149,.T.);
#21537=ORIENTED_EDGE('',*,*,#15117,.F.);
#21538=ORIENTED_EDGE('',*,*,#15116,.F.);
#21539=ORIENTED_EDGE('',*,*,#15146,.T.);
#21540=ORIENTED_EDGE('',*,*,#15153,.F.);
#21541=ORIENTED_EDGE('',*,*,#15151,.T.);
#21542=ORIENTED_EDGE('',*,*,#14936,.T.);
#21543=ORIENTED_EDGE('',*,*,#15154,.T.);
#21544=ORIENTED_EDGE('',*,*,#15138,.T.);
#21545=ORIENTED_EDGE('',*,*,#15036,.F.);
#21546=ORIENTED_EDGE('',*,*,#14942,.T.);
#21547=ORIENTED_EDGE('',*,*,#15155,.T.);
#21548=ORIENTED_EDGE('',*,*,#15137,.T.);
#21549=ORIENTED_EDGE('',*,*,#15154,.F.);
#21550=ORIENTED_EDGE('',*,*,#14984,.T.);
#21551=ORIENTED_EDGE('',*,*,#15156,.T.);
#21552=ORIENTED_EDGE('',*,*,#15133,.T.);
#21553=ORIENTED_EDGE('',*,*,#15155,.F.);
#21554=ORIENTED_EDGE('',*,*,#14980,.T.);
#21555=ORIENTED_EDGE('',*,*,#15157,.T.);
#21556=ORIENTED_EDGE('',*,*,#15144,.T.);
#21557=ORIENTED_EDGE('',*,*,#15156,.F.);
#21558=ORIENTED_EDGE('',*,*,#14979,.T.);
#21559=ORIENTED_EDGE('',*,*,#15158,.T.);
#21560=ORIENTED_EDGE('',*,*,#15143,.T.);
#21561=ORIENTED_EDGE('',*,*,#15157,.F.);
#21562=ORIENTED_EDGE('',*,*,#14975,.T.);
#21563=ORIENTED_EDGE('',*,*,#15159,.T.);
#21564=ORIENTED_EDGE('',*,*,#15139,.T.);
#21565=ORIENTED_EDGE('',*,*,#15158,.F.);
#21566=ORIENTED_EDGE('',*,*,#14971,.T.);
#21567=ORIENTED_EDGE('',*,*,#15160,.T.);
#21568=ORIENTED_EDGE('',*,*,#15145,.T.);
#21569=ORIENTED_EDGE('',*,*,#15159,.F.);
#21570=ORIENTED_EDGE('',*,*,#14968,.T.);
#21571=ORIENTED_EDGE('',*,*,#15161,.T.);
#21572=ORIENTED_EDGE('',*,*,#15153,.T.);
#21573=ORIENTED_EDGE('',*,*,#15160,.F.);
#21574=ORIENTED_EDGE('',*,*,#14967,.T.);
#21575=ORIENTED_EDGE('',*,*,#15162,.T.);
#21576=ORIENTED_EDGE('',*,*,#15152,.T.);
#21577=ORIENTED_EDGE('',*,*,#15161,.F.);
#21578=ORIENTED_EDGE('',*,*,#14964,.T.);
#21579=ORIENTED_EDGE('',*,*,#15163,.T.);
#21580=ORIENTED_EDGE('',*,*,#15150,.T.);
#21581=ORIENTED_EDGE('',*,*,#15162,.F.);
#21582=ORIENTED_EDGE('',*,*,#14930,.F.);
#21583=ORIENTED_EDGE('',*,*,#14961,.T.);
#21584=ORIENTED_EDGE('',*,*,#15164,.T.);
#21585=ORIENTED_EDGE('',*,*,#15148,.T.);
#21586=ORIENTED_EDGE('',*,*,#15163,.F.);
#21587=ORIENTED_EDGE('',*,*,#14958,.T.);
#21588=ORIENTED_EDGE('',*,*,#15165,.T.);
#21589=ORIENTED_EDGE('',*,*,#15122,.T.);
#21590=ORIENTED_EDGE('',*,*,#15164,.F.);
#21591=ORIENTED_EDGE('',*,*,#14955,.T.);
#21592=ORIENTED_EDGE('',*,*,#15166,.T.);
#21593=ORIENTED_EDGE('',*,*,#15167,.F.);
#21594=ORIENTED_EDGE('',*,*,#15168,.F.);
#21595=ORIENTED_EDGE('',*,*,#15124,.T.);
#21596=ORIENTED_EDGE('',*,*,#15165,.F.);
#21597=ORIENTED_EDGE('',*,*,#15089,.T.);
#21598=ORIENTED_EDGE('',*,*,#15168,.T.);
#21599=ORIENTED_EDGE('',*,*,#15169,.F.);
#21600=ORIENTED_EDGE('',*,*,#15170,.T.);
#21601=ORIENTED_EDGE('',*,*,#15079,.T.);
#21602=ORIENTED_EDGE('',*,*,#15064,.T.);
#21603=ORIENTED_EDGE('',*,*,#15171,.F.);
#21604=ORIENTED_EDGE('',*,*,#15056,.T.);
#21605=ORIENTED_EDGE('',*,*,#15063,.T.);
#21606=ORIENTED_EDGE('',*,*,#15061,.T.);
#21607=ORIENTED_EDGE('',*,*,#15059,.T.);
#21608=ORIENTED_EDGE('',*,*,#15057,.T.);
#21609=ORIENTED_EDGE('',*,*,#15171,.T.);
#21610=ORIENTED_EDGE('',*,*,#15172,.T.);
#21611=ORIENTED_EDGE('',*,*,#15173,.T.);
#21612=ORIENTED_EDGE('',*,*,#15174,.T.);
#21613=ORIENTED_EDGE('',*,*,#15169,.T.);
#21614=ORIENTED_EDGE('',*,*,#15167,.T.);
#21615=ORIENTED_EDGE('',*,*,#14952,.T.);
#21616=ORIENTED_EDGE('',*,*,#15175,.T.);
#21617=ORIENTED_EDGE('',*,*,#15172,.F.);
#21618=ORIENTED_EDGE('',*,*,#15166,.F.);
#21619=ORIENTED_EDGE('',*,*,#14949,.T.);
#21620=ORIENTED_EDGE('',*,*,#15176,.T.);
#21621=ORIENTED_EDGE('',*,*,#15173,.F.);
#21622=ORIENTED_EDGE('',*,*,#15175,.F.);
#21623=ORIENTED_EDGE('',*,*,#14944,.T.);
#21624=ORIENTED_EDGE('',*,*,#15177,.T.);
#21625=ORIENTED_EDGE('',*,*,#15095,.T.);
#21626=ORIENTED_EDGE('',*,*,#15170,.F.);
#21627=ORIENTED_EDGE('',*,*,#15174,.F.);
#21628=ORIENTED_EDGE('',*,*,#15176,.F.);
#21629=ORIENTED_EDGE('',*,*,#15035,.T.);
#21630=ORIENTED_EDGE('',*,*,#15074,.T.);
#21631=ORIENTED_EDGE('',*,*,#15097,.T.);
#21632=ORIENTED_EDGE('',*,*,#15177,.F.);
#26473=PLANE('',#28935);
#26474=PLANE('',#28939);
#26475=PLANE('',#29028);
#26476=PLANE('',#29031);
#26477=PLANE('',#29032);
#26478=PLANE('',#29033);
#26479=PLANE('',#29036);
#26480=PLANE('',#29039);
#26481=PLANE('',#29043);
#26482=PLANE('',#29046);
#26483=PLANE('',#29049);
#26484=PLANE('',#29050);
#26485=PLANE('',#29051);
#26486=PLANE('',#29052);
#26487=PLANE('',#29076);
#26488=PLANE('',#29127);
#26489=PLANE('',#29128);
#26490=PLANE('',#29129);
#26491=PLANE('',#29130);
#26492=PLANE('',#29132);
#26493=PLANE('',#29133);
#26494=PLANE('',#29134);
#26495=PLANE('',#29136);
#26496=PLANE('',#29138);
#26497=PLANE('',#29145);
#26498=PLANE('',#29146);
#26499=PLANE('',#29148);
#26500=PLANE('',#29150);
#27292=ADVANCED_FACE('',(#3489),#2506,.F.);
#27293=ADVANCED_FACE('',(#3490),#26473,.T.);
#27294=ADVANCED_FACE('',(#3491),#2507,.F.);
#27295=ADVANCED_FACE('',(#3492),#26474,.F.);
#27296=ADVANCED_FACE('',(#3493),#2508,.T.);
#27297=ADVANCED_FACE('',(#3494),#2509,.T.);
#27298=ADVANCED_FACE('',(#3495),#2510,.T.);
#27299=ADVANCED_FACE('',(#3496),#79,.T.);
#27300=ADVANCED_FACE('',(#3497),#2511,.T.);
#27301=ADVANCED_FACE('',(#3498),#80,.T.);
#27302=ADVANCED_FACE('',(#3499),#2512,.T.);
#27303=ADVANCED_FACE('',(#3500),#81,.T.);
#27304=ADVANCED_FACE('',(#3501),#2513,.T.);
#27305=ADVANCED_FACE('',(#3502),#59,.F.);
#27306=ADVANCED_FACE('',(#3503),#2514,.T.);
#27307=ADVANCED_FACE('',(#3504),#2515,.T.);
#27308=ADVANCED_FACE('',(#3505),#2516,.T.);
#27309=ADVANCED_FACE('',(#3506),#82,.T.);
#27310=ADVANCED_FACE('',(#3507),#2517,.T.);
#27311=ADVANCED_FACE('',(#3508),#2518,.T.);
#27312=ADVANCED_FACE('',(#3509),#2519,.T.);
#27313=ADVANCED_FACE('',(#3510),#83,.T.);
#27314=ADVANCED_FACE('',(#3511),#2520,.T.);
#27315=ADVANCED_FACE('',(#3512),#2521,.T.);
#27316=ADVANCED_FACE('',(#3513),#2522,.T.);
#27317=ADVANCED_FACE('',(#3514),#60,.F.);
#27318=ADVANCED_FACE('',(#3515),#2523,.T.);
#27319=ADVANCED_FACE('',(#3516),#84,.T.);
#27320=ADVANCED_FACE('',(#3517),#2524,.T.);
#27321=ADVANCED_FACE('',(#3518),#85,.T.);
#27322=ADVANCED_FACE('',(#3519),#2525,.T.);
#27323=ADVANCED_FACE('',(#3520),#86,.T.);
#27324=ADVANCED_FACE('',(#3521),#2526,.T.);
#27325=ADVANCED_FACE('',(#3522),#2527,.T.);
#27326=ADVANCED_FACE('',(#3523),#2528,.T.);
#27327=ADVANCED_FACE('',(#3524),#2529,.T.);
#27328=ADVANCED_FACE('',(#3525),#51,.T.);
#27329=ADVANCED_FACE('',(#3526),#52,.T.);
#27330=ADVANCED_FACE('',(#3527),#26475,.F.);
#27331=ADVANCED_FACE('',(#3528),#2530,.F.);
#27332=ADVANCED_FACE('',(#3529),#26476,.F.);
#27333=ADVANCED_FACE('',(#3530),#26477,.F.);
#27334=ADVANCED_FACE('',(#3531),#26478,.F.);
#27335=ADVANCED_FACE('',(#3532),#2531,.T.);
#27336=ADVANCED_FACE('',(#3533,#202),#26479,.F.);
#27337=ADVANCED_FACE('',(#3534),#2532,.T.);
#27338=ADVANCED_FACE('',(#3535),#26480,.F.);
#27339=ADVANCED_FACE('',(#3536),#2533,.T.);
#27340=ADVANCED_FACE('',(#3537),#26481,.F.);
#27341=ADVANCED_FACE('',(#3538),#2534,.F.);
#27342=ADVANCED_FACE('',(#3539),#26482,.F.);
#27343=ADVANCED_FACE('',(#3540),#2535,.T.);
#27344=ADVANCED_FACE('',(#3541),#26483,.F.);
#27345=ADVANCED_FACE('',(#3542),#26484,.F.);
#27346=ADVANCED_FACE('',(#3543),#26485,.F.);
#27347=ADVANCED_FACE('',(#3544),#26486,.T.);
#27348=ADVANCED_FACE('',(#3545),#2536,.T.);
#27349=ADVANCED_FACE('',(#3546),#87,.T.);
#27350=ADVANCED_FACE('',(#3547),#2537,.T.);
#27351=ADVANCED_FACE('',(#3548),#2538,.T.);
#27352=ADVANCED_FACE('',(#3549),#2539,.T.);
#27353=ADVANCED_FACE('',(#3550),#53,.T.);
#27354=ADVANCED_FACE('',(#3551),#88,.T.);
#27355=ADVANCED_FACE('',(#3552),#2540,.T.);
#27356=ADVANCED_FACE('',(#3553),#54,.T.);
#27357=ADVANCED_FACE('',(#3554),#2541,.T.);
#27358=ADVANCED_FACE('',(#3555),#26487,.F.);
#27359=ADVANCED_FACE('',(#3556),#2542,.T.);
#27360=ADVANCED_FACE('',(#3557),#89,.T.);
#27361=ADVANCED_FACE('',(#3558),#2543,.T.);
#27362=ADVANCED_FACE('',(#3559),#61,.F.);
#27363=ADVANCED_FACE('',(#3560),#2544,.T.);
#27364=ADVANCED_FACE('',(#3561),#90,.T.);
#27365=ADVANCED_FACE('',(#3562),#91,.T.);
#27366=ADVANCED_FACE('',(#3563),#2545,.T.);
#27367=ADVANCED_FACE('',(#3564),#2546,.T.);
#27368=ADVANCED_FACE('',(#3565),#92,.T.);
#27369=ADVANCED_FACE('',(#3566),#2547,.T.);
#27370=ADVANCED_FACE('',(#3567),#2548,.T.);
#27371=ADVANCED_FACE('',(#3568),#2549,.T.);
#27372=ADVANCED_FACE('',(#3569),#2550,.T.);
#27373=ADVANCED_FACE('',(#3570),#2551,.T.);
#27374=ADVANCED_FACE('',(#3571),#93,.T.);
#27375=ADVANCED_FACE('',(#3572),#2552,.T.);
#27376=ADVANCED_FACE('',(#3573),#2553,.T.);
#27377=ADVANCED_FACE('',(#3574),#94,.T.);
#27378=ADVANCED_FACE('',(#3575),#2554,.T.);
#27379=ADVANCED_FACE('',(#3576),#62,.F.);
#27380=ADVANCED_FACE('',(#3577),#2555,.T.);
#27381=ADVANCED_FACE('',(#3578),#26488,.F.);
#27382=ADVANCED_FACE('',(#3579),#26489,.F.);
#27383=ADVANCED_FACE('',(#3580),#26490,.F.);
#27384=ADVANCED_FACE('',(#3581),#26491,.F.);
#27385=ADVANCED_FACE('',(#3582),#2556,.F.);
#27386=ADVANCED_FACE('',(#3583),#26492,.F.);
#27387=ADVANCED_FACE('',(#3584),#26493,.F.);
#27388=ADVANCED_FACE('',(#3585),#26494,.F.);
#27389=ADVANCED_FACE('',(#3586),#2557,.T.);
#27390=ADVANCED_FACE('',(#3587,#203),#26495,.F.);
#27391=ADVANCED_FACE('',(#3588),#2558,.T.);
#27392=ADVANCED_FACE('',(#3589),#26496,.F.);
#27393=ADVANCED_FACE('',(#3590),#2559,.T.);
#27394=ADVANCED_FACE('',(#3591),#2560,.F.);
#27395=ADVANCED_FACE('',(#3592),#2561,.F.);
#27396=ADVANCED_FACE('',(#3593),#26497,.F.);
#27397=ADVANCED_FACE('',(#3594),#26498,.F.);
#27398=ADVANCED_FACE('',(#3595),#26499,.F.);
#27399=ADVANCED_FACE('',(#3596),#2562,.F.);
#27400=ADVANCED_FACE('',(#3597),#26500,.F.);
#27401=ADVANCED_FACE('',(#3598),#2563,.T.);
#28084=CLOSED_SHELL('',(#27292,#27293,#27294,#27295,#27296,#27297,#27298,
#27299,#27300,#27301,#27302,#27303,#27304,#27305,#27306,#27307,#27308,#27309,
#27310,#27311,#27312,#27313,#27314,#27315,#27316,#27317,#27318,#27319,#27320,
#27321,#27322,#27323,#27324,#27325,#27326,#27327,#27328,#27329,#27330,#27331,
#27332,#27333,#27334,#27335,#27336,#27337,#27338,#27339,#27340,#27341,#27342,
#27343,#27344,#27345,#27346,#27347,#27348,#27349,#27350,#27351,#27352,#27353,
#27354,#27355,#27356,#27357,#27358,#27359,#27360,#27361,#27362,#27363,#27364,
#27365,#27366,#27367,#27368,#27369,#27370,#27371,#27372,#27373,#27374,#27375,
#27376,#27377,#27378,#27379,#27380,#27381,#27382,#27383,#27384,#27385,#27386,
#27387,#27388,#27389,#27390,#27391,#27392,#27393,#27394,#27395,#27396,#27397,
#27398,#27399,#27400,#27401));
#28931=AXIS2_PLACEMENT_3D('',#125023,#32334,#32335);
#28932=AXIS2_PLACEMENT_3D('',#125024,#32336,#32337);
#28933=AXIS2_PLACEMENT_3D('',#125026,#32338,#32339);
#28934=AXIS2_PLACEMENT_3D('',#125029,#32341,#32342);
#28935=AXIS2_PLACEMENT_3D('',#125030,#32343,#32344);
#28936=AXIS2_PLACEMENT_3D('',#125031,#32345,#32346);
#28937=AXIS2_PLACEMENT_3D('',#125033,#32347,#32348);
#28938=AXIS2_PLACEMENT_3D('',#125036,#32350,#32351);
#28939=AXIS2_PLACEMENT_3D('',#125037,#32352,#32353);
#28940=AXIS2_PLACEMENT_3D('',#125038,#32354,#32355);
#28941=AXIS2_PLACEMENT_3D('',#125043,#32357,#32358);
#28942=AXIS2_PLACEMENT_3D('',#125046,#32360,#32361);
#28943=AXIS2_PLACEMENT_3D('',#125047,#32362,#32363);
#28944=AXIS2_PLACEMENT_3D('',#125051,#32365,#32366);
#28945=AXIS2_PLACEMENT_3D('',#125053,#32368,#32369);
#28946=AXIS2_PLACEMENT_3D('',#125056,#32370,#32371);
#28947=AXIS2_PLACEMENT_3D('',#125060,#32373,#32374);
#28948=AXIS2_PLACEMENT_3D('',#125062,#32376,#32377);
#28949=AXIS2_PLACEMENT_3D('',#125065,#32378,#32379);
#28950=AXIS2_PLACEMENT_3D('',#125066,#32380,#32381);
#28951=AXIS2_PLACEMENT_3D('',#125067,#32382,#32383);
#28952=AXIS2_PLACEMENT_3D('',#125068,#32384,#32385);
#28953=AXIS2_PLACEMENT_3D('',#125071,#32386,#32387);
#28954=AXIS2_PLACEMENT_3D('',#125074,#32390,#32391);
#28955=AXIS2_PLACEMENT_3D('',#125077,#32392,#32393);
#28956=AXIS2_PLACEMENT_3D('',#125078,#32394,#32395);
#28957=AXIS2_PLACEMENT_3D('',#125079,#32396,#32397);
#28958=AXIS2_PLACEMENT_3D('',#125080,#32398,#32399);
#28959=AXIS2_PLACEMENT_3D('',#125083,#32400,#32401);
#28960=AXIS2_PLACEMENT_3D('',#125086,#32404,#32405);
#28961=AXIS2_PLACEMENT_3D('',#125089,#32406,#32407);
#28962=AXIS2_PLACEMENT_3D('',#125090,#32408,#32409);
#28963=AXIS2_PLACEMENT_3D('',#125091,#32410,#32411);
#28964=AXIS2_PLACEMENT_3D('',#125092,#32412,#32413);
#28965=AXIS2_PLACEMENT_3D('',#125095,#32414,#32415);
#28966=AXIS2_PLACEMENT_3D('',#125109,#32418,#32419);
#28967=AXIS2_PLACEMENT_3D('',#125110,#32420,#32421);
#28968=AXIS2_PLACEMENT_3D('',#125111,#32422,#32423);
#28969=AXIS2_PLACEMENT_3D('',#125112,#32424,#32425);
#28970=AXIS2_PLACEMENT_3D('',#125116,#32427,#32428);
#28971=AXIS2_PLACEMENT_3D('',#125118,#32430,#32431);
#28972=AXIS2_PLACEMENT_3D('',#125122,#32433,#32434);
#28973=AXIS2_PLACEMENT_3D('',#125124,#32436,#32437);
#28974=AXIS2_PLACEMENT_3D('',#125129,#32440,#32441);
#28975=AXIS2_PLACEMENT_3D('',#125130,#32442,#32443);
#28976=AXIS2_PLACEMENT_3D('',#125133,#32444,#32445);
#28977=AXIS2_PLACEMENT_3D('',#125134,#32446,#32447);
#28978=AXIS2_PLACEMENT_3D('',#125135,#32448,#32449);
#28979=AXIS2_PLACEMENT_3D('',#125136,#32450,#32451);
#28980=AXIS2_PLACEMENT_3D('',#125140,#32453,#32454);
#28981=AXIS2_PLACEMENT_3D('',#125142,#32456,#32457);
#28982=AXIS2_PLACEMENT_3D('',#125145,#32460,#32461);
#28983=AXIS2_PLACEMENT_3D('',#125150,#32464,#32465);
#28984=AXIS2_PLACEMENT_3D('',#125151,#32466,#32467);
#28985=AXIS2_PLACEMENT_3D('',#125154,#32468,#32469);
#28986=AXIS2_PLACEMENT_3D('',#125155,#32470,#32471);
#28987=AXIS2_PLACEMENT_3D('',#125156,#32472,#32473);
#28988=AXIS2_PLACEMENT_3D('',#125157,#32474,#32475);
#28989=AXIS2_PLACEMENT_3D('',#125161,#32477,#32478);
#28990=AXIS2_PLACEMENT_3D('',#125163,#32480,#32481);
#28991=AXIS2_PLACEMENT_3D('',#125168,#32484,#32485);
#28992=AXIS2_PLACEMENT_3D('',#125169,#32486,#32487);
#28993=AXIS2_PLACEMENT_3D('',#125174,#32490,#32491);
#28994=AXIS2_PLACEMENT_3D('',#125186,#32492,#32493);
#28995=AXIS2_PLACEMENT_3D('',#125187,#32494,#32495);
#28996=AXIS2_PLACEMENT_3D('',#125188,#32496,#32497);
#28997=AXIS2_PLACEMENT_3D('',#125189,#32498,#32499);
#28998=AXIS2_PLACEMENT_3D('',#125192,#32500,#32501);
#28999=AXIS2_PLACEMENT_3D('',#125195,#32504,#32505);
#29000=AXIS2_PLACEMENT_3D('',#125198,#32506,#32507);
#29001=AXIS2_PLACEMENT_3D('',#125199,#32508,#32509);
#29002=AXIS2_PLACEMENT_3D('',#125200,#32510,#32511);
#29003=AXIS2_PLACEMENT_3D('',#125201,#32512,#32513);
#29004=AXIS2_PLACEMENT_3D('',#125204,#32514,#32515);
#29005=AXIS2_PLACEMENT_3D('',#125207,#32518,#32519);
#29006=AXIS2_PLACEMENT_3D('',#125210,#32520,#32521);
#29007=AXIS2_PLACEMENT_3D('',#125211,#32522,#32523);
#29008=AXIS2_PLACEMENT_3D('',#125212,#32524,#32525);
#29009=AXIS2_PLACEMENT_3D('',#125213,#32526,#32527);
#29010=AXIS2_PLACEMENT_3D('',#125216,#32528,#32529);
#29011=AXIS2_PLACEMENT_3D('',#125219,#32532,#32533);
#29012=AXIS2_PLACEMENT_3D('',#125222,#32534,#32535);
#29013=AXIS2_PLACEMENT_3D('',#125223,#32536,#32537);
#29014=AXIS2_PLACEMENT_3D('',#125224,#32538,#32539);
#29015=AXIS2_PLACEMENT_3D('',#125225,#32540,#32541);
#29016=AXIS2_PLACEMENT_3D('',#125228,#32542,#32543);
#29017=AXIS2_PLACEMENT_3D('',#125231,#32546,#32547);
#29018=AXIS2_PLACEMENT_3D('',#125234,#32548,#32549);
#29019=AXIS2_PLACEMENT_3D('',#125237,#32551,#32552);
#29020=AXIS2_PLACEMENT_3D('',#125239,#32554,#32555);
#29021=AXIS2_PLACEMENT_3D('',#125243,#32557,#32558);
#29022=AXIS2_PLACEMENT_3D('',#125245,#32560,#32561);
#29023=AXIS2_PLACEMENT_3D('',#125248,#32563,#32564);
#29024=AXIS2_PLACEMENT_3D('',#125250,#32566,#32567);
#29025=AXIS2_PLACEMENT_3D('',#125251,#32568,#32569);
#29026=AXIS2_PLACEMENT_3D('',#125252,#32570,#32571);
#29027=AXIS2_PLACEMENT_3D('',#125253,#32572,#32573);
#29028=AXIS2_PLACEMENT_3D('',#125254,#32574,#32575);
#29029=AXIS2_PLACEMENT_3D('',#125260,#32579,#32580);
#29030=AXIS2_PLACEMENT_3D('',#125262,#32581,#32582);
#29031=AXIS2_PLACEMENT_3D('',#125264,#32584,#32585);
#29032=AXIS2_PLACEMENT_3D('',#125268,#32588,#32589);
#29033=AXIS2_PLACEMENT_3D('',#125272,#32592,#32593);
#29034=AXIS2_PLACEMENT_3D('',#125276,#32596,#32597);
#29035=AXIS2_PLACEMENT_3D('',#125278,#32598,#32599);
#29036=AXIS2_PLACEMENT_3D('',#125280,#32601,#32602);
#29037=AXIS2_PLACEMENT_3D('',#125284,#32605,#32606);
#29038=AXIS2_PLACEMENT_3D('',#125286,#32607,#32608);
#29039=AXIS2_PLACEMENT_3D('',#125288,#32610,#32611);
#29040=AXIS2_PLACEMENT_3D('',#125292,#32614,#32615);
#29041=AXIS2_PLACEMENT_3D('',#125294,#32616,#32617);
#29042=AXIS2_PLACEMENT_3D('',#125298,#32619,#32620);
#29043=AXIS2_PLACEMENT_3D('',#125300,#32622,#32623);
#29044=AXIS2_PLACEMENT_3D('',#125304,#32626,#32627);
#29045=AXIS2_PLACEMENT_3D('',#125306,#32628,#32629);
#29046=AXIS2_PLACEMENT_3D('',#125308,#32631,#32632);
#29047=AXIS2_PLACEMENT_3D('',#125316,#32637,#32638);
#29048=AXIS2_PLACEMENT_3D('',#125318,#32639,#32640);
#29049=AXIS2_PLACEMENT_3D('',#125320,#32642,#32643);
#29050=AXIS2_PLACEMENT_3D('',#125324,#32646,#32647);
#29051=AXIS2_PLACEMENT_3D('',#125328,#32650,#32651);
#29052=AXIS2_PLACEMENT_3D('',#125332,#32654,#32655);
#29053=AXIS2_PLACEMENT_3D('',#125333,#32656,#32657);
#29054=AXIS2_PLACEMENT_3D('',#125351,#32659,#32660);
#29055=AXIS2_PLACEMENT_3D('',#125352,#32661,#32662);
#29056=AXIS2_PLACEMENT_3D('',#125354,#32663,#32664);
#29057=AXIS2_PLACEMENT_3D('',#125355,#32665,#32666);
#29058=AXIS2_PLACEMENT_3D('',#125377,#32667,#32668);
#29059=AXIS2_PLACEMENT_3D('',#125379,#32669,#32670);
#29060=AXIS2_PLACEMENT_3D('',#125380,#32671,#32672);
#29061=AXIS2_PLACEMENT_3D('',#125382,#32674,#32675);
#29062=AXIS2_PLACEMENT_3D('',#125384,#32676,#32677);
#29063=AXIS2_PLACEMENT_3D('',#125386,#32679,#32680);
#29064=AXIS2_PLACEMENT_3D('',#125389,#32682,#32683);
#29065=AXIS2_PLACEMENT_3D('',#125390,#32684,#32685);
#29066=AXIS2_PLACEMENT_3D('',#125391,#32686,#32687);
#29067=AXIS2_PLACEMENT_3D('',#125394,#32688,#32689);
#29068=AXIS2_PLACEMENT_3D('',#125411,#32690,#32691);
#29069=AXIS2_PLACEMENT_3D('',#125433,#32692,#32693);
#29070=AXIS2_PLACEMENT_3D('',#125437,#32696,#32697);
#29071=AXIS2_PLACEMENT_3D('',#125438,#32698,#32699);
#29072=AXIS2_PLACEMENT_3D('',#125439,#32700,#32701);
#29073=AXIS2_PLACEMENT_3D('',#125440,#32702,#32703);
#29074=AXIS2_PLACEMENT_3D('',#125441,#32704,#32705);
#29075=AXIS2_PLACEMENT_3D('',#125443,#32706,#32707);
#29076=AXIS2_PLACEMENT_3D('',#125445,#32709,#32710);
#29077=AXIS2_PLACEMENT_3D('',#125447,#32711,#32712);
#29078=AXIS2_PLACEMENT_3D('',#125451,#32714,#32715);
#29079=AXIS2_PLACEMENT_3D('',#125459,#32719,#32720);
#29080=AXIS2_PLACEMENT_3D('',#125471,#32726,#32727);
#29081=AXIS2_PLACEMENT_3D('',#125479,#32731,#32732);
#29082=AXIS2_PLACEMENT_3D('',#125483,#32734,#32735);
#29083=AXIS2_PLACEMENT_3D('',#125485,#32737,#32738);
#29084=AXIS2_PLACEMENT_3D('',#125487,#32739,#32740);
#29085=AXIS2_PLACEMENT_3D('',#125490,#32742,#32743);
#29086=AXIS2_PLACEMENT_3D('',#125491,#32744,#32745);
#29087=AXIS2_PLACEMENT_3D('',#125492,#32746,#32747);
#29088=AXIS2_PLACEMENT_3D('',#125493,#32748,#32749);
#29089=AXIS2_PLACEMENT_3D('',#125494,#32750,#32751);
#29090=AXIS2_PLACEMENT_3D('',#125495,#32752,#32753);
#29091=AXIS2_PLACEMENT_3D('',#125505,#32754,#32755);
#29092=AXIS2_PLACEMENT_3D('',#125506,#32756,#32757);
#29093=AXIS2_PLACEMENT_3D('',#125507,#32758,#32759);
#29094=AXIS2_PLACEMENT_3D('',#125508,#32760,#32761);
#29095=AXIS2_PLACEMENT_3D('',#125509,#32762,#32763);
#29096=AXIS2_PLACEMENT_3D('',#125510,#32764,#32765);
#29097=AXIS2_PLACEMENT_3D('',#125511,#32766,#32767);
#29098=AXIS2_PLACEMENT_3D('',#125512,#32768,#32769);
#29099=AXIS2_PLACEMENT_3D('',#125513,#32770,#32771);
#29100=AXIS2_PLACEMENT_3D('',#125514,#32772,#32773);
#29101=AXIS2_PLACEMENT_3D('',#125515,#32774,#32775);
#29102=AXIS2_PLACEMENT_3D('',#125516,#32776,#32777);
#29103=AXIS2_PLACEMENT_3D('',#125517,#32778,#32779);
#29104=AXIS2_PLACEMENT_3D('',#125518,#32780,#32781);
#29105=AXIS2_PLACEMENT_3D('',#125522,#32783,#32784);
#29106=AXIS2_PLACEMENT_3D('',#125523,#32785,#32786);
#29107=AXIS2_PLACEMENT_3D('',#125524,#32787,#32788);
#29108=AXIS2_PLACEMENT_3D('',#125526,#32789,#32790);
#29109=AXIS2_PLACEMENT_3D('',#125528,#32792,#32793);
#29110=AXIS2_PLACEMENT_3D('',#125530,#32795,#32796);
#29111=AXIS2_PLACEMENT_3D('',#125534,#32798,#32799);
#29112=AXIS2_PLACEMENT_3D('',#125535,#32800,#32801);
#29113=AXIS2_PLACEMENT_3D('',#125536,#32802,#32803);
#29114=AXIS2_PLACEMENT_3D('',#125538,#32804,#32805);
#29115=AXIS2_PLACEMENT_3D('',#125539,#32806,#32807);
#29116=AXIS2_PLACEMENT_3D('',#125540,#32808,#32809);
#29117=AXIS2_PLACEMENT_3D('',#125542,#32811,#32812);
#29118=AXIS2_PLACEMENT_3D('',#125545,#32814,#32815);
#29119=AXIS2_PLACEMENT_3D('',#125546,#32816,#32817);
#29120=AXIS2_PLACEMENT_3D('',#125548,#32818,#32819);
#29121=AXIS2_PLACEMENT_3D('',#125549,#32820,#32821);
#29122=AXIS2_PLACEMENT_3D('',#125550,#32822,#32823);
#29123=AXIS2_PLACEMENT_3D('',#125552,#32824,#32825);
#29124=AXIS2_PLACEMENT_3D('',#125564,#32827,#32828);
#29125=AXIS2_PLACEMENT_3D('',#125565,#32829,#32830);
#29126=AXIS2_PLACEMENT_3D('',#125566,#32831,#32832);
#29127=AXIS2_PLACEMENT_3D('',#125568,#32834,#32835);
#29128=AXIS2_PLACEMENT_3D('',#125570,#32837,#32838);
#29129=AXIS2_PLACEMENT_3D('',#125572,#32840,#32841);
#29130=AXIS2_PLACEMENT_3D('',#125574,#32843,#32844);
#29131=AXIS2_PLACEMENT_3D('',#125576,#32846,#32847);
#29132=AXIS2_PLACEMENT_3D('',#125578,#32849,#32850);
#29133=AXIS2_PLACEMENT_3D('',#125580,#32852,#32853);
#29134=AXIS2_PLACEMENT_3D('',#125582,#32855,#32856);
#29135=AXIS2_PLACEMENT_3D('',#125584,#32858,#32859);
#29136=AXIS2_PLACEMENT_3D('',#125586,#32861,#32862);
#29137=AXIS2_PLACEMENT_3D('',#125588,#32864,#32865);
#29138=AXIS2_PLACEMENT_3D('',#125590,#32867,#32868);
#29139=AXIS2_PLACEMENT_3D('',#125592,#32870,#32871);
#29140=AXIS2_PLACEMENT_3D('',#125596,#32873,#32874);
#29141=AXIS2_PLACEMENT_3D('',#125598,#32876,#32877);
#29142=AXIS2_PLACEMENT_3D('',#125600,#32878,#32879);
#29143=AXIS2_PLACEMENT_3D('',#125602,#32881,#32882);
#29144=AXIS2_PLACEMENT_3D('',#125603,#32883,#32884);
#29145=AXIS2_PLACEMENT_3D('',#125604,#32885,#32886);
#29146=AXIS2_PLACEMENT_3D('',#125605,#32887,#32888);
#29147=AXIS2_PLACEMENT_3D('',#125609,#32890,#32891);
#29148=AXIS2_PLACEMENT_3D('',#125611,#32893,#32894);
#29149=AXIS2_PLACEMENT_3D('',#125613,#32896,#32897);
#29150=AXIS2_PLACEMENT_3D('',#125615,#32899,#32900);
#29151=AXIS2_PLACEMENT_3D('',#125617,#32902,#32903);
#32334=DIRECTION('axis',(0.,0.,1.));
#32335=DIRECTION('refdir',(1.,0.,0.));
#32336=DIRECTION('center_axis',(-1.,-6.57957785206009E-13,0.));
#32337=DIRECTION('ref_axis',(0.,0.,-1.));
#32338=DIRECTION('center_axis',(1.,-3.28954970259306E-16,0.));
#32339=DIRECTION('ref_axis',(0.,0.,-1.));
#32340=DIRECTION('',(-1.,-6.57957785206009E-13,0.));
#32341=DIRECTION('center_axis',(-1.,-6.58286732145141E-13,0.));
#32342=DIRECTION('ref_axis',(0.,0.,-1.));
#32343=DIRECTION('center_axis',(1.,6.58286732145141E-13,0.));
#32344=DIRECTION('ref_axis',(0.,0.,-1.));
#32345=DIRECTION('center_axis',(-0.999999999362884,3.56963971004376E-5,
0.));
#32346=DIRECTION('ref_axis',(0.,0.,-1.));
#32347=DIRECTION('center_axis',(-0.999999999362884,3.56963971007665E-5,
0.));
#32348=DIRECTION('ref_axis',(0.,0.,-1.));
#32349=DIRECTION('',(-0.999999999362884,3.56963971004376E-5,0.));
#32350=DIRECTION('center_axis',(-0.999999999362884,3.56963971007665E-5,
0.));
#32351=DIRECTION('ref_axis',(0.,0.,-1.));
#32352=DIRECTION('center_axis',(0.999999999362884,-3.56963971007665E-5,
0.));
#32353=DIRECTION('ref_axis',(0.,0.,-1.));
#32354=DIRECTION('center_axis',(0.999999999362884,-3.56963971010297E-5,
0.));
#32355=DIRECTION('ref_axis',(-2.52411644540658E-5,-0.707106780736035,-0.707106781186551));
#32356=DIRECTION('',(0.999999999362884,-3.56963971010297E-5,0.));
#32357=DIRECTION('center_axis',(-0.970304361397857,-0.24188725938399,0.));
#32358=DIRECTION('ref_axis',(0.24188725938399,-0.970304361397857,0.));
#32359=DIRECTION('',(-0.999999999362884,3.56963971010297E-5,0.));
#32360=DIRECTION('center_axis',(0.999999999362884,-3.56963970959969E-5,
0.));
#32361=DIRECTION('ref_axis',(-3.56963970959969E-5,-0.999999999362884,0.));
#32362=DIRECTION('center_axis',(-0.999999999840721,1.7848198553344E-5,0.));
#32363=DIRECTION('ref_axis',(-1.26205822290334E-5,-0.707106781073918,-0.70710678118655));
#32364=DIRECTION('',(-0.999999999840721,1.7848198553344E-5,0.));
#32365=DIRECTION('center_axis',(0.999999999840721,-1.78481985546597E-5,
0.));
#32366=DIRECTION('ref_axis',(-1.78481985546597E-5,-0.999999999840721,0.));
#32367=DIRECTION('',(0.999999999840721,-1.7848198553344E-5,0.));
#32368=DIRECTION('center_axis',(0.,1.,0.));
#32369=DIRECTION('ref_axis',(0.707106781186548,0.,-0.707106781186548));
#32370=DIRECTION('center_axis',(0.,1.,0.));
#32371=DIRECTION('ref_axis',(1.,0.,0.));
#32372=DIRECTION('',(0.,1.,0.));
#32373=DIRECTION('center_axis',(0.,-1.,0.));
#32374=DIRECTION('ref_axis',(0.,0.,-1.));
#32375=DIRECTION('',(0.,-1.,0.));
#32376=DIRECTION('center_axis',(0.,0.,1.));
#32377=DIRECTION('ref_axis',(-1.,0.,0.));
#32378=DIRECTION('center_axis',(1.,0.,0.));
#32379=DIRECTION('ref_axis',(0.,0.,-1.));
#32380=DIRECTION('center_axis',(0.,0.,1.));
#32381=DIRECTION('ref_axis',(-0.707106781186545,-0.70710678118655,0.));
#32382=DIRECTION('center_axis',(0.,0.,-1.));
#32383=DIRECTION('ref_axis',(-0.707106781186545,-0.70710678118655,0.));
#32384=DIRECTION('center_axis',(-1.,0.,0.));
#32385=DIRECTION('ref_axis',(0.,0.707106781186548,-0.707106781186548));
#32386=DIRECTION('center_axis',(1.,0.,0.));
#32387=DIRECTION('ref_axis',(0.,0.,-1.));
#32388=DIRECTION('',(1.,0.,0.));
#32389=DIRECTION('',(-1.,0.,0.));
#32390=DIRECTION('center_axis',(0.,0.,1.));
#32391=DIRECTION('ref_axis',(-1.,0.,0.));
#32392=DIRECTION('center_axis',(0.707106781186545,-0.70710678118655,0.));
#32393=DIRECTION('ref_axis',(0.,0.,-1.));
#32394=DIRECTION('center_axis',(0.,0.,-1.));
#32395=DIRECTION('ref_axis',(0.382683432365091,0.923879532511286,0.));
#32396=DIRECTION('center_axis',(0.,0.,1.));
#32397=DIRECTION('ref_axis',(0.382683432365091,0.923879532511286,0.));
#32398=DIRECTION('center_axis',(-0.707106781186548,0.707106781186547,0.));
#32399=DIRECTION('ref_axis',(0.5,0.500000000000001,-0.707106781186547));
#32400=DIRECTION('center_axis',(0.707106781186548,-0.707106781186548,0.));
#32401=DIRECTION('ref_axis',(0.,0.,-1.));
#32402=DIRECTION('',(0.707106781186548,-0.707106781186547,0.));
#32403=DIRECTION('',(-0.707106781186548,0.707106781186547,0.));
#32404=DIRECTION('center_axis',(0.,0.,1.));
#32405=DIRECTION('ref_axis',(-1.,0.,0.));
#32406=DIRECTION('center_axis',(0.,-1.,0.));
#32407=DIRECTION('ref_axis',(0.,0.,-1.));
#32408=DIRECTION('center_axis',(0.,0.,-1.));
#32409=DIRECTION('ref_axis',(0.923879532511287,0.38268343236509,0.));
#32410=DIRECTION('center_axis',(0.,0.,1.));
#32411=DIRECTION('ref_axis',(0.923879532511287,0.38268343236509,0.));
#32412=DIRECTION('center_axis',(3.28954970259306E-16,1.,0.));
#32413=DIRECTION('ref_axis',(0.707106781186548,-2.32606290175374E-16,-0.707106781186548));
#32414=DIRECTION('center_axis',(0.,-1.,0.));
#32415=DIRECTION('ref_axis',(0.,0.,-1.));
#32416=DIRECTION('',(-3.28954970259306E-16,-1.,0.));
#32417=DIRECTION('',(3.28954970259306E-16,1.,0.));
#32418=DIRECTION('center_axis',(-1.,0.,0.));
#32419=DIRECTION('ref_axis',(0.,0.,-1.));
#32420=DIRECTION('center_axis',(0.,0.,-1.));
#32421=DIRECTION('ref_axis',(0.707106781186547,-0.707106781186548,0.));
#32422=DIRECTION('center_axis',(0.,0.,1.));
#32423=DIRECTION('ref_axis',(0.707106781186546,-0.707106781186549,0.));
#32424=DIRECTION('center_axis',(1.,0.,0.));
#32425=DIRECTION('ref_axis',(0.,-0.707106781186548,-0.707106781186548));
#32426=DIRECTION('',(1.,0.,0.));
#32427=DIRECTION('center_axis',(-0.92387953251129,0.382683432365083,0.));
#32428=DIRECTION('ref_axis',(0.382683432365083,0.92387953251129,0.));
#32429=DIRECTION('',(-1.,0.,0.));
#32430=DIRECTION('center_axis',(0.707106781186548,-0.707106781186547,0.));
#32431=DIRECTION('ref_axis',(-0.499999999999999,-0.499999999999999,-0.707106781186549));
#32432=DIRECTION('',(0.707106781186548,-0.707106781186547,0.));
#32433=DIRECTION('center_axis',(-0.382683432365083,0.92387953251129,0.));
#32434=DIRECTION('ref_axis',(0.92387953251129,0.382683432365083,0.));
#32435=DIRECTION('',(-0.707106781186548,0.707106781186547,0.));
#32436=DIRECTION('center_axis',(0.,-1.,0.));
#32437=DIRECTION('ref_axis',(-0.707106781186551,0.,-0.707106781186544));
#32438=DIRECTION('',(0.,1.,0.));
#32439=DIRECTION('',(0.,-1.,0.));
#32440=DIRECTION('center_axis',(0.,1.,0.));
#32441=DIRECTION('ref_axis',(0.,0.,-1.));
#32442=DIRECTION('center_axis',(0.,0.,1.));
#32443=DIRECTION('ref_axis',(-1.,0.,0.));
#32444=DIRECTION('center_axis',(-0.88294759285893,0.469471562785885,0.));
#32445=DIRECTION('ref_axis',(0.,0.,-1.));
#32446=DIRECTION('center_axis',(0.,0.,1.));
#32447=DIRECTION('ref_axis',(0.857167300702112,0.515038074910055,0.));
#32448=DIRECTION('center_axis',(0.,0.,-1.));
#32449=DIRECTION('ref_axis',(0.857167300702112,0.515038074910055,0.));
#32450=DIRECTION('center_axis',(0.882947592858928,-0.46947156278589,0.));
#32451=DIRECTION('ref_axis',(-0.331966525620151,-0.624338230342891,-0.707106781186542));
#32452=DIRECTION('',(0.882947592858928,-0.46947156278589,0.));
#32453=DIRECTION('center_axis',(-0.970295726275989,0.241921895599697,0.));
#32454=DIRECTION('ref_axis',(-0.241921895599697,-0.970295726275989,0.));
#32455=DIRECTION('',(-0.882947592858928,0.46947156278589,0.));
#32456=DIRECTION('center_axis',(1.,0.,0.));
#32457=DIRECTION('ref_axis',(0.,-0.707106781186548,-0.707106781186548));
#32458=DIRECTION('',(-1.,0.,0.));
#32459=DIRECTION('',(1.,0.,0.));
#32460=DIRECTION('center_axis',(0.882964350739721,0.469440044438886,0.));
#32461=DIRECTION('ref_axis',(0.331944238783253,-0.624350079954038,-0.707106781186543));
#32462=DIRECTION('',(-0.882964350739721,-0.469440044438886,0.));
#32463=DIRECTION('',(0.882964350739721,0.469440044438886,0.));
#32464=DIRECTION('center_axis',(-0.882964350739719,-0.46944004443889,0.));
#32465=DIRECTION('ref_axis',(0.,0.,-1.));
#32466=DIRECTION('center_axis',(0.,0.,1.));
#32467=DIRECTION('ref_axis',(-1.,0.,0.));
#32468=DIRECTION('center_axis',(-3.56963971004376E-5,-0.999999999362884,
0.));
#32469=DIRECTION('ref_axis',(0.,0.,-1.));
#32470=DIRECTION('center_axis',(0.,0.,1.));
#32471=DIRECTION('ref_axis',(-0.857148915152355,0.51506867236626,0.));
#32472=DIRECTION('center_axis',(0.,0.,-1.));
#32473=DIRECTION('ref_axis',(-0.857148915152355,0.51506867236626,0.));
#32474=DIRECTION('center_axis',(3.56963971014961E-5,0.999999999362884,0.));
#32475=DIRECTION('ref_axis',(0.707106780736038,-2.52411644543957E-5,-0.707106781186548));
#32476=DIRECTION('',(3.56963971014961E-5,0.999999999362884,0.));
#32477=DIRECTION('center_axis',(-0.382716411291948,-0.9238658715029,0.));
#32478=DIRECTION('ref_axis',(-0.9238658715029,0.382716411291948,0.));
#32479=DIRECTION('',(-3.56963971014961E-5,-0.999999999362884,0.));
#32480=DIRECTION('center_axis',(0.707132021900493,0.707081539571584,0.));
#32481=DIRECTION('ref_axis',(0.499982151482891,-0.500017847879993,-0.707106781186548));
#32482=DIRECTION('',(-0.707132021900493,-0.707081539571584,0.));
#32483=DIRECTION('',(0.707132021900493,0.707081539571584,0.));
#32484=DIRECTION('center_axis',(-0.923893192342431,-0.382650452950617,-6.50651058246798E-15));
#32485=DIRECTION('ref_axis',(-0.382650452950617,0.923893192342431,-1.57081060919186E-14));
#32486=DIRECTION('center_axis',(0.999999999362884,-3.5696397100931E-5,0.));
#32487=DIRECTION('ref_axis',(-2.52411644539961E-5,-0.707106780736038,-0.707106781186548));
#32488=DIRECTION('',(-0.999999999362884,3.5696397100931E-5,0.));
#32489=DIRECTION('',(0.999999999362884,-3.5696397100931E-5,0.));
#32490=DIRECTION('center_axis',(-0.999999999362884,3.56963971004377E-5,
0.));
#32491=DIRECTION('ref_axis',(0.,0.,-1.));
#32492=DIRECTION('center_axis',(3.56963971048783E-5,0.999999999362884,0.));
#32493=DIRECTION('ref_axis',(0.,0.,-1.));
#32494=DIRECTION('center_axis',(0.,0.,-1.));
#32495=DIRECTION('ref_axis',(-0.707132021900492,-0.707081539571584,0.));
#32496=DIRECTION('center_axis',(0.,0.,1.));
#32497=DIRECTION('ref_axis',(-0.707132021900492,-0.707081539571584,0.));
#32498=DIRECTION('center_axis',(-3.56963971007665E-5,-0.999999999362884,
0.));
#32499=DIRECTION('ref_axis',(-0.707106780736035,2.52411644538797E-5,-0.707106781186551));
#32500=DIRECTION('center_axis',(3.56963971004377E-5,0.999999999362884,0.));
#32501=DIRECTION('ref_axis',(0.,0.,-1.));
#32502=DIRECTION('',(3.56963971007665E-5,0.999999999362884,0.));
#32503=DIRECTION('',(-3.56963971007665E-5,-0.999999999362884,0.));
#32504=DIRECTION('center_axis',(0.,0.,1.));
#32505=DIRECTION('ref_axis',(-1.,0.,0.));
#32506=DIRECTION('center_axis',(0.707132021900495,0.707081539571582,0.));
#32507=DIRECTION('ref_axis',(0.,0.,-1.));
#32508=DIRECTION('center_axis',(0.,0.,-1.));
#32509=DIRECTION('ref_axis',(-0.923865871502902,0.382716411291943,0.));
#32510=DIRECTION('center_axis',(0.,0.,1.));
#32511=DIRECTION('ref_axis',(-0.923865871502902,0.382716411291943,0.));
#32512=DIRECTION('center_axis',(-0.707132021900493,-0.707081539571584,0.));
#32513=DIRECTION('ref_axis',(-0.499982151482891,0.500017847879993,-0.707106781186548));
#32514=DIRECTION('center_axis',(0.70713202190049,0.707081539571586,0.));
#32515=DIRECTION('ref_axis',(0.,0.,-1.));
#32516=DIRECTION('',(0.707132021900493,0.707081539571584,0.));
#32517=DIRECTION('',(-0.707132021900493,-0.707081539571584,0.));
#32518=DIRECTION('center_axis',(0.,0.,1.));
#32519=DIRECTION('ref_axis',(-1.,0.,0.));
#32520=DIRECTION('center_axis',(0.999999999362884,-3.56963971004377E-5,
0.));
#32521=DIRECTION('ref_axis',(0.,0.,-1.));
#32522=DIRECTION('center_axis',(0.,0.,-1.));
#32523=DIRECTION('ref_axis',(-0.382650452950611,0.923893192342433,0.));
#32524=DIRECTION('center_axis',(0.,0.,1.));
#32525=DIRECTION('ref_axis',(-0.382650452950611,0.923893192342433,0.));
#32526=DIRECTION('center_axis',(-0.999999999362884,3.56963971021026E-5,
0.));
#32527=DIRECTION('ref_axis',(2.52411644548245E-5,0.707106780736035,-0.707106781186551));
#32528=DIRECTION('center_axis',(0.999999999362884,-3.5696397104879E-5,0.));
#32529=DIRECTION('ref_axis',(0.,0.,-1.));
#32530=DIRECTION('',(0.999999999362884,-3.56963971021026E-5,0.));
#32531=DIRECTION('',(-0.999999999362884,3.56963971021026E-5,0.));
#32532=DIRECTION('center_axis',(0.,0.,1.));
#32533=DIRECTION('ref_axis',(-1.,0.,0.));
#32534=DIRECTION('center_axis',(3.56963971004376E-5,0.999999999362884,0.));
#32535=DIRECTION('ref_axis',(0.,0.,-1.));
#32536=DIRECTION('center_axis',(0.,0.,1.));
#32537=DIRECTION('ref_axis',(0.707081539571586,-0.70713202190049,0.));
#32538=DIRECTION('center_axis',(0.,0.,-1.));
#32539=DIRECTION('ref_axis',(0.707081539571587,-0.70713202190049,0.));
#32540=DIRECTION('center_axis',(-3.56963971011028E-5,-0.999999999362884,
0.));
#32541=DIRECTION('ref_axis',(-0.707106780736038,2.52411644541176E-5,-0.707106781186548));
#32542=DIRECTION('center_axis',(3.56963970915558E-5,0.999999999362884,0.));
#32543=DIRECTION('ref_axis',(0.,0.,-1.));
#32544=DIRECTION('',(3.56963971011028E-5,0.999999999362884,0.));
#32545=DIRECTION('',(-3.56963971011028E-5,-0.999999999362884,0.));
#32546=DIRECTION('center_axis',(-1.,0.,0.));
#32547=DIRECTION('ref_axis',(0.,0.707106781186554,-0.707106781186541));
#32548=DIRECTION('center_axis',(-1.,0.,0.));
#32549=DIRECTION('ref_axis',(0.,1.,0.));
#32550=DIRECTION('',(-1.,0.,0.));
#32551=DIRECTION('center_axis',(1.,0.,0.));
#32552=DIRECTION('ref_axis',(0.,0.,-1.));
#32553=DIRECTION('',(1.,0.,0.));
#32554=DIRECTION('center_axis',(0.999999999840721,-1.78481985534681E-5,
0.));
#32555=DIRECTION('ref_axis',(1.26205822291212E-5,0.707106781073918,-0.70710678118655));
#32556=DIRECTION('',(0.999999999840721,-1.78481985534681E-5,0.));
#32557=DIRECTION('center_axis',(-0.999999999840721,1.78481985546596E-5,
0.));
#32558=DIRECTION('ref_axis',(1.78481985546596E-5,0.999999999840721,0.));
#32559=DIRECTION('',(-0.999999999840721,1.78481985534681E-5,0.));
#32560=DIRECTION('center_axis',(-0.999999999362884,3.56963971040562E-5,
0.));
#32561=DIRECTION('ref_axis',(2.52411644562058E-5,0.707106780736035,-0.707106781186551));
#32562=DIRECTION('',(0.999999999362884,-3.56963971040562E-5,0.));
#32563=DIRECTION('center_axis',(-0.999999999362884,3.5696397104879E-5,0.));
#32564=DIRECTION('ref_axis',(3.5696397104879E-5,0.999999999362884,0.));
#32565=DIRECTION('',(-0.999999999362884,3.56963971040562E-5,0.));
#32566=DIRECTION('center_axis',(-0.816511153790762,-0.408241003122002,0.408226431169298));
#32567=DIRECTION('ref_axis',(-0.577329659497308,0.577370878146268,-0.577350269189622));
#32568=DIRECTION('center_axis',(0.,0.,1.));
#32569=DIRECTION('ref_axis',(-0.999999999362884,3.56963970915558E-5,0.));
#32570=DIRECTION('center_axis',(0.408248290463868,-0.816496580927721,-0.408248290463868));
#32571=DIRECTION('ref_axis',(0.577350269189616,0.577350269189634,-0.577350269189627));
#32572=DIRECTION('center_axis',(0.,0.,1.));
#32573=DIRECTION('ref_axis',(-4.44089209850064E-15,1.,0.));
#32574=DIRECTION('center_axis',(-0.469440044438886,0.882964350739721,0.));
#32575=DIRECTION('ref_axis',(-0.882964350739721,-0.469440044438886,0.));
#32576=DIRECTION('',(0.,0.,1.));
#32577=DIRECTION('',(-0.882964350739721,-0.469440044438886,0.));
#32578=DIRECTION('',(0.,0.,1.));
#32579=DIRECTION('center_axis',(0.,0.,-1.));
#32580=DIRECTION('ref_axis',(-0.999999999362884,3.56963971004376E-5,0.));
#32581=DIRECTION('center_axis',(0.,0.,1.));
#32582=DIRECTION('ref_axis',(-0.857148915152355,0.51506867236626,0.));
#32583=DIRECTION('',(0.,0.,1.));
#32584=DIRECTION('center_axis',(-0.999999999362884,3.56963971014961E-5,
0.));
#32585=DIRECTION('ref_axis',(-3.56963971014961E-5,-0.999999999362884,0.));
#32586=DIRECTION('',(-3.56963971014961E-5,-0.999999999362884,0.));
#32587=DIRECTION('',(0.,0.,1.));
#32588=DIRECTION('center_axis',(-0.707081539571584,0.707132021900493,0.));
#32589=DIRECTION('ref_axis',(-0.707132021900493,-0.707081539571584,0.));
#32590=DIRECTION('',(-0.707132021900493,-0.707081539571584,0.));
#32591=DIRECTION('',(0.,0.,1.));
#32592=DIRECTION('center_axis',(3.5696397100931E-5,0.999999999362884,0.));
#32593=DIRECTION('ref_axis',(-0.999999999362884,3.5696397100931E-5,0.));
#32594=DIRECTION('',(-0.999999999362884,3.5696397100931E-5,0.));
#32595=DIRECTION('',(0.,0.,1.));
#32596=DIRECTION('center_axis',(0.,0.,-1.));
#32597=DIRECTION('ref_axis',(-3.56963971004376E-5,-0.999999999362884,0.));
#32598=DIRECTION('center_axis',(0.,0.,-1.));
#32599=DIRECTION('ref_axis',(-0.707132021900492,-0.707081539571584,0.));
#32600=DIRECTION('',(0.,0.,1.));
#32601=DIRECTION('center_axis',(0.999999999362884,-3.56963971007665E-5,
0.));
#32602=DIRECTION('ref_axis',(3.56963971007665E-5,0.999999999362884,0.));
#32603=DIRECTION('',(3.56963971007665E-5,0.999999999362884,0.));
#32604=DIRECTION('',(0.,0.,1.));
#32605=DIRECTION('center_axis',(0.,0.,-1.));
#32606=DIRECTION('ref_axis',(-0.999999999362884,3.56963971013258E-5,0.));
#32607=DIRECTION('center_axis',(0.,0.,-1.));
#32608=DIRECTION('ref_axis',(-0.923865871502902,0.382716411291943,0.));
#32609=DIRECTION('',(0.,0.,1.));
#32610=DIRECTION('center_axis',(0.707081539571584,-0.707132021900493,0.));
#32611=DIRECTION('ref_axis',(0.707132021900493,0.707081539571584,0.));
#32612=DIRECTION('',(0.707132021900493,0.707081539571584,0.));
#32613=DIRECTION('',(0.,0.,1.));
#32614=DIRECTION('center_axis',(0.,0.,-1.));
#32615=DIRECTION('ref_axis',(-0.707081539571585,0.707132021900492,0.));
#32616=DIRECTION('center_axis',(0.,0.,-1.));
#32617=DIRECTION('ref_axis',(-0.674257203707391,0.738496596639883,0.));
#32618=DIRECTION('',(0.,0.,1.));
#32619=DIRECTION('center_axis',(0.,0.,1.));
#32620=DIRECTION('ref_axis',(-0.707081539571585,0.707132021900492,0.));
#32621=DIRECTION('',(0.,0.,1.));
#32622=DIRECTION('center_axis',(-3.56963971021026E-5,-0.999999999362884,
0.));
#32623=DIRECTION('ref_axis',(0.999999999362884,-3.56963971021026E-5,0.));
#32624=DIRECTION('',(-0.999999999362884,3.56963971021026E-5,0.));
#32625=DIRECTION('',(0.,0.,1.));
#32626=DIRECTION('center_axis',(0.,0.,-1.));
#32627=DIRECTION('ref_axis',(0.999999999362884,-3.56963970980596E-5,0.));
#32628=DIRECTION('center_axis',(0.,0.,-1.));
#32629=DIRECTION('ref_axis',(0.999999999362884,-3.56963970980596E-5,0.));
#32630=DIRECTION('',(0.,0.,1.));
#32631=DIRECTION('center_axis',(0.999999999362884,-3.56963971011028E-5,
0.));
#32632=DIRECTION('ref_axis',(3.56963971011028E-5,0.999999999362884,0.));
#32633=DIRECTION('',(-3.56963971011028E-5,-0.999999999362884,0.));
#32634=DIRECTION('',(0.,0.,-1.));
#32635=DIRECTION('',(3.56963971011028E-5,0.999999999362884,0.));
#32636=DIRECTION('',(0.,0.,1.));
#32637=DIRECTION('center_axis',(0.,0.,-1.));
#32638=DIRECTION('ref_axis',(-0.999999999362884,3.56963970915558E-5,0.));
#32639=DIRECTION('center_axis',(0.,0.,-1.));
#32640=DIRECTION('ref_axis',(-0.999999999362884,3.56963970915558E-5,0.));
#32641=DIRECTION('',(0.,0.,1.));
#32642=DIRECTION('center_axis',(-3.56963971040562E-5,-0.999999999362884,
0.));
#32643=DIRECTION('ref_axis',(0.999999999362884,-3.56963971040562E-5,0.));
#32644=DIRECTION('',(0.999999999362884,-3.56963971040562E-5,0.));
#32645=DIRECTION('',(0.,0.,1.));
#32646=DIRECTION('center_axis',(-1.78481985534681E-5,-0.999999999840721,
0.));
#32647=DIRECTION('ref_axis',(0.999999999840721,-1.78481985534681E-5,0.));
#32648=DIRECTION('',(0.999999999840721,-1.78481985534681E-5,0.));
#32649=DIRECTION('',(0.,0.,1.));
#32650=DIRECTION('center_axis',(0.,-1.,0.));
#32651=DIRECTION('ref_axis',(1.,0.,0.));
#32652=DIRECTION('',(1.,0.,0.));
#32653=DIRECTION('',(0.,0.,1.));
#32654=DIRECTION('center_axis',(0.,0.,-1.));
#32655=DIRECTION('ref_axis',(-1.,0.,0.));
#32656=DIRECTION('center_axis',(-3.56963971011028E-5,-0.999999999362884,
0.));
#32657=DIRECTION('ref_axis',(-0.707106780736038,2.52411644541176E-5,0.707106781186548));
#32658=DIRECTION('',(-3.56963971011028E-5,-0.999999999362884,0.));
#32659=DIRECTION('center_axis',(3.56963970915558E-5,0.999999999362884,0.));
#32660=DIRECTION('ref_axis',(-0.999999999362884,3.56963970915558E-5,0.));
#32661=DIRECTION('center_axis',(0.,0.,-1.));
#32662=DIRECTION('ref_axis',(1.,0.,0.));
#32663=DIRECTION('center_axis',(0.,0.,-1.));
#32664=DIRECTION('ref_axis',(0.880581945986775,-0.473893908382608,0.));
#32665=DIRECTION('center_axis',(0.,0.,1.));
#32666=DIRECTION('ref_axis',(0.880581945986775,-0.473893908382608,0.));
#32667=DIRECTION('center_axis',(-0.999999999362884,3.56963971040562E-5,
0.));
#32668=DIRECTION('ref_axis',(2.52411644562058E-5,0.707106780736035,0.707106781186551));
#32669=DIRECTION('center_axis',(0.999999999362884,-3.56963971004374E-5,
0.));
#32670=DIRECTION('ref_axis',(3.56963971004374E-5,0.999999999362884,0.));
#32671=DIRECTION('center_axis',(-0.999999999362884,3.56963971048783E-5,
0.));
#32672=DIRECTION('ref_axis',(0.,0.,1.));
#32673=DIRECTION('',(-0.999999999362884,3.56963971040562E-5,0.));
#32674=DIRECTION('center_axis',(-0.999999999840721,1.78481985534681E-5,
0.));
#32675=DIRECTION('ref_axis',(1.26205822291212E-5,0.707106781073918,0.70710678118655));
#32676=DIRECTION('center_axis',(0.999999999840721,-1.78481985457778E-5,
0.));
#32677=DIRECTION('ref_axis',(1.78481985457778E-5,0.999999999840721,0.));
#32678=DIRECTION('',(-0.999999999840721,1.78481985534681E-5,0.));
#32679=DIRECTION('center_axis',(-1.,0.,0.));
#32680=DIRECTION('ref_axis',(0.,0.707106781186554,0.707106781186541));
#32681=DIRECTION('',(-1.,0.,0.));
#32682=DIRECTION('center_axis',(1.,0.,0.));
#32683=DIRECTION('ref_axis',(0.,1.,0.));
#32684=DIRECTION('center_axis',(-0.816511153790763,-0.408241003122,-0.408226431169296));
#32685=DIRECTION('ref_axis',(-0.57732965949731,0.577370878146255,0.577350269189634));
#32686=DIRECTION('center_axis',(0.,0.,-1.));
#32687=DIRECTION('ref_axis',(-0.836963911810301,-0.54725808383906,0.));
#32688=DIRECTION('center_axis',(0.,0.,1.));
#32689=DIRECTION('ref_axis',(-0.880598861730879,-0.473862474477859,0.));
#32690=DIRECTION('center_axis',(0.,0.,-1.));
#32691=DIRECTION('ref_axis',(-0.88059886173088,-0.473862474477859,0.));
#32692=DIRECTION('center_axis',(0.,1.,0.));
#32693=DIRECTION('ref_axis',(0.707106781186548,0.,0.707106781186548));
#32694=DIRECTION('',(0.,1.,0.));
#32695=DIRECTION('',(0.,-1.,0.));
#32696=DIRECTION('center_axis',(0.,1.,0.));
#32697=DIRECTION('ref_axis',(0.,0.,1.));
#32698=DIRECTION('center_axis',(0.408248290463864,-0.816496580927721,0.408248290463871));
#32699=DIRECTION('ref_axis',(0.577350269189621,0.577350269189625,0.577350269189632));
#32700=DIRECTION('center_axis',(0.,0.,-1.));
#32701=DIRECTION('ref_axis',(-4.44089209850064E-15,1.,0.));
#32702=DIRECTION('center_axis',(-0.707132021900493,-0.707081539571584,0.));
#32703=DIRECTION('ref_axis',(-0.499982151482891,0.500017847879993,0.707106781186548));
#32704=DIRECTION('center_axis',(0.70713202190049,0.707081539571586,0.));
#32705=DIRECTION('ref_axis',(-0.707081539571586,0.70713202190049,0.));
#32706=DIRECTION('center_axis',(0.707132021900495,0.707081539571582,0.));
#32707=DIRECTION('ref_axis',(-0.707081539571582,0.707132021900495,0.));
#32708=DIRECTION('',(-0.707132021900493,-0.707081539571584,0.));
#32709=DIRECTION('center_axis',(0.,0.,-1.));
#32710=DIRECTION('ref_axis',(-1.,0.,0.));
#32711=DIRECTION('center_axis',(0.,0.,1.));
#32712=DIRECTION('ref_axis',(-0.923865871502902,0.382716411291943,0.));
#32713=DIRECTION('',(-3.56963971007665E-5,-0.999999999362884,0.));
#32714=DIRECTION('center_axis',(0.,0.,1.));
#32715=DIRECTION('ref_axis',(-0.707132021900492,-0.707081539571584,0.));
#32716=DIRECTION('',(0.999999999362884,-3.5696397100931E-5,0.));
#32717=DIRECTION('',(0.707132021900493,0.707081539571584,0.));
#32718=DIRECTION('',(3.56963971014961E-5,0.999999999362884,0.));
#32719=DIRECTION('center_axis',(0.,0.,-1.));
#32720=DIRECTION('ref_axis',(-0.857148915152355,0.51506867236626,0.));
#32721=DIRECTION('',(0.882964350739721,0.469440044438886,0.));
#32722=DIRECTION('',(0.999999999362884,-3.56963971010297E-5,0.));
#32723=DIRECTION('',(0.999999999840721,-1.7848198553344E-5,0.));
#32724=DIRECTION('',(1.,0.,0.));
#32725=DIRECTION('',(0.882947592858928,-0.46947156278589,0.));
#32726=DIRECTION('center_axis',(0.,0.,-1.));
#32727=DIRECTION('ref_axis',(0.857167300702112,0.515038074910055,0.));
#32728=DIRECTION('',(0.,-1.,0.));
#32729=DIRECTION('',(0.707106781186548,-0.707106781186547,0.));
#32730=DIRECTION('',(1.,0.,0.));
#32731=DIRECTION('center_axis',(0.,0.,1.));
#32732=DIRECTION('ref_axis',(0.707106781186547,-0.707106781186548,0.));
#32733=DIRECTION('',(3.28954970259306E-16,1.,0.));
#32734=DIRECTION('center_axis',(0.,0.,1.));
#32735=DIRECTION('ref_axis',(0.923879532511287,0.38268343236509,0.));
#32736=DIRECTION('',(-0.707106781186548,0.707106781186547,0.));
#32737=DIRECTION('center_axis',(-0.707106781186548,0.707106781186547,0.));
#32738=DIRECTION('ref_axis',(0.5,0.500000000000001,0.707106781186547));
#32739=DIRECTION('center_axis',(0.707106781186548,-0.707106781186548,0.));
#32740=DIRECTION('ref_axis',(0.707106781186548,0.707106781186548,0.));
#32741=DIRECTION('',(0.707106781186548,-0.707106781186547,0.));
#32742=DIRECTION('center_axis',(0.707106781186548,-0.707106781186548,0.));
#32743=DIRECTION('ref_axis',(0.707106781186548,0.707106781186548,0.));
#32744=DIRECTION('center_axis',(0.,0.,1.));
#32745=DIRECTION('ref_axis',(-1.,0.,0.));
#32746=DIRECTION('center_axis',(0.,0.,-1.));
#32747=DIRECTION('ref_axis',(0.674283564945582,0.738472527616483,0.));
#32748=DIRECTION('center_axis',(0.999999999362884,-3.5696397100931E-5,0.));
#32749=DIRECTION('ref_axis',(-2.52411644539961E-5,-0.707106780736038,0.707106781186548));
#32750=DIRECTION('center_axis',(0.923893192342434,0.38265045295061,-1.69930937299605E-15));
#32751=DIRECTION('ref_axis',(0.38265045295061,-0.923893192342434,4.10249573495478E-15));
#32752=DIRECTION('center_axis',(-0.999999999362884,3.56963971004376E-5,
0.));
#32753=DIRECTION('ref_axis',(-3.56963971004376E-5,-0.999999999362884,0.));
#32754=DIRECTION('center_axis',(3.56963971048783E-5,0.999999999362884,0.));
#32755=DIRECTION('ref_axis',(-0.999999999362884,3.56963971048783E-5,0.));
#32756=DIRECTION('center_axis',(-3.56963971007665E-5,-0.999999999362884,
0.));
#32757=DIRECTION('ref_axis',(-0.707106780736035,2.52411644538797E-5,0.707106781186551));
#32758=DIRECTION('center_axis',(3.56963971004377E-5,0.999999999362884,0.));
#32759=DIRECTION('ref_axis',(-0.999999999362884,3.56963971004377E-5,0.));
#32760=DIRECTION('center_axis',(0.,0.,1.));
#32761=DIRECTION('ref_axis',(-1.,0.,0.));
#32762=DIRECTION('center_axis',(0.,0.,1.));
#32763=DIRECTION('ref_axis',(-1.,0.,0.));
#32764=DIRECTION('center_axis',(0.707132021900493,0.707081539571584,0.));
#32765=DIRECTION('ref_axis',(0.499982151482891,-0.500017847879993,0.707106781186548));
#32766=DIRECTION('center_axis',(0.382716411291948,0.9238658715029,-4.10278864883162E-15));
#32767=DIRECTION('ref_axis',(0.9238658715029,-0.382716411291948,9.90500799955984E-15));
#32768=DIRECTION('center_axis',(0.882964350739721,0.469440044438886,0.));
#32769=DIRECTION('ref_axis',(0.33194423878325,-0.624350079954033,0.707106781186549));
#32770=DIRECTION('center_axis',(0.970304361397861,0.241887259383973,0.));
#32771=DIRECTION('ref_axis',(-0.241887259383973,0.970304361397861,0.));
#32772=DIRECTION('center_axis',(-0.88296435073972,-0.469440044438887,0.));
#32773=DIRECTION('ref_axis',(0.469440044438887,-0.88296435073972,0.));
#32774=DIRECTION('center_axis',(0.,0.,-1.));
#32775=DIRECTION('ref_axis',(1.,0.,0.));
#32776=DIRECTION('center_axis',(-3.56963971004376E-5,-0.999999999362884,
0.));
#32777=DIRECTION('ref_axis',(0.999999999362884,-3.56963971004376E-5,0.));
#32778=DIRECTION('center_axis',(3.56963971014961E-5,0.999999999362884,0.));
#32779=DIRECTION('ref_axis',(0.707106780736038,-2.52411644543957E-5,0.707106781186548));
#32780=DIRECTION('center_axis',(1.,0.,0.));
#32781=DIRECTION('ref_axis',(0.,-0.707106781186548,0.707106781186548));
#32782=DIRECTION('',(-1.,0.,0.));
#32783=DIRECTION('center_axis',(0.970295726275993,-0.241921895599681,0.));
#32784=DIRECTION('ref_axis',(0.241921895599681,0.970295726275993,0.));
#32785=DIRECTION('center_axis',(-1.,0.,0.));
#32786=DIRECTION('ref_axis',(0.,-1.,0.));
#32787=DIRECTION('center_axis',(0.999999999840721,-1.7848198553344E-5,0.));
#32788=DIRECTION('ref_axis',(-1.26205822290334E-5,-0.707106781073918,0.70710678118655));
#32789=DIRECTION('center_axis',(-0.999999999840721,1.78481985502188E-5,
0.));
#32790=DIRECTION('ref_axis',(-1.78481985502188E-5,-0.999999999840721,0.));
#32791=DIRECTION('',(-0.999999999840721,1.7848198553344E-5,0.));
#32792=DIRECTION('center_axis',(0.999999999362884,-3.56963971010297E-5,
0.));
#32793=DIRECTION('ref_axis',(-2.52411644540658E-5,-0.707106780736035,0.707106781186551));
#32794=DIRECTION('',(-0.999999999362884,3.56963971010297E-5,0.));
#32795=DIRECTION('center_axis',(0.,-1.,0.));
#32796=DIRECTION('ref_axis',(-0.707106781186551,0.,0.707106781186544));
#32797=DIRECTION('',(0.,1.,0.));
#32798=DIRECTION('center_axis',(0.382683432365083,-0.92387953251129,0.));
#32799=DIRECTION('ref_axis',(-0.92387953251129,-0.382683432365083,0.));
#32800=DIRECTION('center_axis',(0.,1.,0.));
#32801=DIRECTION('ref_axis',(-1.,0.,0.));
#32802=DIRECTION('center_axis',(0.,0.,-1.));
#32803=DIRECTION('ref_axis',(1.,0.,0.));
#32804=DIRECTION('center_axis',(-0.88294759285893,0.469471562785885,0.));
#32805=DIRECTION('ref_axis',(-0.469471562785885,-0.88294759285893,0.));
#32806=DIRECTION('center_axis',(0.,0.,1.));
#32807=DIRECTION('ref_axis',(0.857167300702112,0.515038074910055,0.));
#32808=DIRECTION('center_axis',(0.882947592858928,-0.46947156278589,0.));
#32809=DIRECTION('ref_axis',(-0.331966525620151,-0.624338230342891,0.707106781186542));
#32810=DIRECTION('',(-0.882947592858928,0.46947156278589,0.));
#32811=DIRECTION('center_axis',(0.707106781186548,-0.707106781186547,0.));
#32812=DIRECTION('ref_axis',(-0.5,-0.500000000000001,0.707106781186547));
#32813=DIRECTION('',(-0.707106781186548,0.707106781186547,0.));
#32814=DIRECTION('center_axis',(0.92387953251129,-0.382683432365083,0.));
#32815=DIRECTION('ref_axis',(-0.382683432365083,-0.92387953251129,0.));
#32816=DIRECTION('center_axis',(0.,0.,1.));
#32817=DIRECTION('ref_axis',(-1.,0.,0.));
#32818=DIRECTION('center_axis',(0.,-1.,0.));
#32819=DIRECTION('ref_axis',(1.,0.,0.));
#32820=DIRECTION('center_axis',(0.,0.,-1.));
#32821=DIRECTION('ref_axis',(0.923879532511287,0.38268343236509,0.));
#32822=DIRECTION('center_axis',(3.28954970259306E-16,1.,0.));
#32823=DIRECTION('ref_axis',(0.707106781186548,-2.32606290175374E-16,0.707106781186548));
#32824=DIRECTION('center_axis',(0.,-1.,0.));
#32825=DIRECTION('ref_axis',(1.,0.,0.));
#32826=DIRECTION('',(-3.28954970259306E-16,-1.,0.));
#32827=DIRECTION('center_axis',(-1.,0.,0.));
#32828=DIRECTION('ref_axis',(0.,-1.,0.));
#32829=DIRECTION('center_axis',(0.,0.,-1.));
#32830=DIRECTION('ref_axis',(0.707106781186546,-0.707106781186549,0.));
#32831=DIRECTION('center_axis',(1.,0.,0.));
#32832=DIRECTION('ref_axis',(0.,-0.707106781186548,0.707106781186548));
#32833=DIRECTION('',(-1.,0.,0.));
#32834=DIRECTION('center_axis',(3.56963971010297E-5,0.999999999362884,0.));
#32835=DIRECTION('ref_axis',(-0.999999999362884,3.56963971010297E-5,0.));
#32836=DIRECTION('',(0.,0.,1.));
#32837=DIRECTION('center_axis',(1.7848198553344E-5,0.999999999840721,0.));
#32838=DIRECTION('ref_axis',(-0.999999999840721,1.7848198553344E-5,0.));
#32839=DIRECTION('',(0.,0.,1.));
#32840=DIRECTION('center_axis',(0.,1.,0.));
#32841=DIRECTION('ref_axis',(-1.,0.,0.));
#32842=DIRECTION('',(0.,0.,1.));
#32843=DIRECTION('center_axis',(0.46947156278589,0.882947592858928,0.));
#32844=DIRECTION('ref_axis',(-0.882947592858928,0.46947156278589,0.));
#32845=DIRECTION('',(0.,0.,1.));
#32846=DIRECTION('center_axis',(0.,0.,-1.));
#32847=DIRECTION('ref_axis',(0.469471562785885,0.88294759285893,0.));
#32848=DIRECTION('',(0.,0.,1.));
#32849=DIRECTION('center_axis',(1.,0.,0.));
#32850=DIRECTION('ref_axis',(0.,1.,0.));
#32851=DIRECTION('',(0.,0.,1.));
#32852=DIRECTION('center_axis',(0.707106781186547,0.707106781186548,0.));
#32853=DIRECTION('ref_axis',(-0.707106781186548,0.707106781186547,0.));
#32854=DIRECTION('',(0.,0.,1.));
#32855=DIRECTION('center_axis',(0.,1.,0.));
#32856=DIRECTION('ref_axis',(-1.,0.,0.));
#32857=DIRECTION('',(0.,0.,1.));
#32858=DIRECTION('center_axis',(0.,0.,-1.));
#32859=DIRECTION('ref_axis',(1.,0.,0.));
#32860=DIRECTION('',(0.,0.,1.));
#32861=DIRECTION('center_axis',(-1.,3.28954970259306E-16,0.));
#32862=DIRECTION('ref_axis',(-3.28954970259306E-16,-1.,0.));
#32863=DIRECTION('',(0.,0.,1.));
#32864=DIRECTION('center_axis',(0.,0.,-1.));
#32865=DIRECTION('ref_axis',(0.707106781186547,0.707106781186548,0.));
#32866=DIRECTION('',(0.,0.,1.));
#32867=DIRECTION('center_axis',(-0.707106781186547,-0.707106781186548,0.));
#32868=DIRECTION('ref_axis',(0.707106781186548,-0.707106781186547,0.));
#32869=DIRECTION('',(0.,0.,1.));
#32870=DIRECTION('center_axis',(0.,0.,-1.));
#32871=DIRECTION('ref_axis',(1.48029736616687E-15,1.,0.));
#32872=DIRECTION('',(0.,0.,1.));
#32873=DIRECTION('center_axis',(0.,0.,1.));
#32874=DIRECTION('ref_axis',(1.48029736616687E-15,1.,0.));
#32875=DIRECTION('',(0.,0.,-1.));
#32876=DIRECTION('center_axis',(0.,0.,1.));
#32877=DIRECTION('ref_axis',(-1.,0.,0.));
#32878=DIRECTION('center_axis',(0.,0.,1.));
#32879=DIRECTION('ref_axis',(-1.,0.,0.));
#32880=DIRECTION('',(0.,0.,1.));
#32881=DIRECTION('center_axis',(0.,0.,1.));
#32882=DIRECTION('ref_axis',(0.836944376135179,-0.547287960086548,0.));
#32883=DIRECTION('center_axis',(0.,0.,1.));
#32884=DIRECTION('ref_axis',(-1.,0.,0.));
#32885=DIRECTION('center_axis',(0.,0.,-1.));
#32886=DIRECTION('ref_axis',(-1.,0.,0.));
#32887=DIRECTION('center_axis',(0.,0.,-1.));
#32888=DIRECTION('ref_axis',(-1.,0.,0.));
#32889=DIRECTION('',(-1.,0.,0.));
#32890=DIRECTION('center_axis',(0.,0.,-1.));
#32891=DIRECTION('ref_axis',(0.,-1.,0.));
#32892=DIRECTION('',(0.,1.,0.));
#32893=DIRECTION('center_axis',(0.,-1.,0.));
#32894=DIRECTION('ref_axis',(1.,0.,0.));
#32895=DIRECTION('',(0.,0.,1.));
#32896=DIRECTION('center_axis',(0.,0.,-1.));
#32897=DIRECTION('ref_axis',(0.,-1.,0.));
#32898=DIRECTION('',(0.,0.,1.));
#32899=DIRECTION('center_axis',(-1.,0.,0.));
#32900=DIRECTION('ref_axis',(0.,-1.,0.));
#32901=DIRECTION('',(0.,0.,1.));
#32902=DIRECTION('center_axis',(0.,0.,-1.));
#32903=DIRECTION('ref_axis',(-4.44089209850064E-15,1.,0.));
#125023=CARTESIAN_POINT('',(0.,0.,0.));
#125024=CARTESIAN_POINT('Origin',(25.9997814655409,18.8808065108639,-21.5));
#125025=CARTESIAN_POINT('',(25.9997805061207,18.8808065108639,-18.5));
#125026=CARTESIAN_POINT('Origin',(25.9997805061207,18.8808065108639,-21.5));
#125027=CARTESIAN_POINT('',(22.9997814655409,18.8808065108619,-18.5));
#125028=CARTESIAN_POINT('',(25.9997814655409,18.8808065108639,-18.5));
#125029=CARTESIAN_POINT('Origin',(22.9997814655409,18.8808065108619,-21.5));
#125030=CARTESIAN_POINT('Origin',(22.9997814655409,18.8808065108619,-21.5));
#125031=CARTESIAN_POINT('Origin',(-26.0001963416363,18.8817346167756,-21.5));
#125032=CARTESIAN_POINT('',(-23.0001963435476,18.8816275275843,-18.5));
#125033=CARTESIAN_POINT('Origin',(-23.0001963435476,18.8816275275843,-21.5));
#125034=CARTESIAN_POINT('',(-26.0001963416363,18.8817346167756,-18.5));
#125035=CARTESIAN_POINT('',(-26.0001963416363,18.8817346167756,-18.5));
#125036=CARTESIAN_POINT('Origin',(-26.0001963416363,18.8817346167756,-21.5));
#125037=CARTESIAN_POINT('Origin',(-23.0001963435476,18.8816275275843,-21.5));
#125038=CARTESIAN_POINT('Origin',(-6.00033197323811,24.630714186474,-25.5));
#125039=CARTESIAN_POINT('',(-15.7502284469069,24.1310622223319,-25.5));
#125040=CARTESIAN_POINT('',(-12.0002284492961,24.1309283608428,-25.5));
#125041=CARTESIAN_POINT('',(-6.00034982143666,24.1307141867926,-25.5));
#125042=CARTESIAN_POINT('',(-15.8748746000505,24.631066672069,-26.));
#125043=CARTESIAN_POINT('Origin',(-15.8748746000505,24.631066672069,-25.5));
#125044=CARTESIAN_POINT('',(-12.0002106010975,24.6309283605242,-26.));
#125045=CARTESIAN_POINT('',(-6.00033197323811,24.630714186474,-26.));
#125046=CARTESIAN_POINT('Origin',(-12.0002106010975,24.6309283605242,-25.5));
#125047=CARTESIAN_POINT('Origin',(5.99980902926158,24.6306070926795,-25.5));
#125048=CARTESIAN_POINT('',(12.0000089240993,24.6304999999204,-26.));
#125049=CARTESIAN_POINT('',(5.99980902926158,24.6306070926795,-26.));
#125050=CARTESIAN_POINT('',(12.,24.1305,-25.5));
#125051=CARTESIAN_POINT('Origin',(12.0000089240993,24.6304999999204,-25.5));
#125052=CARTESIAN_POINT('',(5.9998001051623,24.1306070927591,-25.5));
#125053=CARTESIAN_POINT('Origin',(15.5005576038968,36.3806823573572,-25.5));
#125054=CARTESIAN_POINT('',(16.0005576038968,44.6304565378295,-25.5));
#125055=CARTESIAN_POINT('',(15.5005576038968,44.6304565378295,-26.));
#125056=CARTESIAN_POINT('Origin',(15.5005576038968,44.6304565378295,-25.5));
#125057=CARTESIAN_POINT('',(16.0005576038968,36.1384565378295,-25.5));
#125058=CARTESIAN_POINT('',(16.0005576038968,36.3806823573572,-25.5));
#125059=CARTESIAN_POINT('',(15.5005576038968,36.1384565378295,-26.));
#125060=CARTESIAN_POINT('Origin',(15.5005576038968,36.1384565378295,-25.5));
#125061=CARTESIAN_POINT('',(15.5005576038968,36.3806823573572,-26.));
#125062=CARTESIAN_POINT('Origin',(16.5085576038968,36.1384565378295,-25.5));
#125063=CARTESIAN_POINT('',(16.5085576038968,35.1304565378295,-26.));
#125064=CARTESIAN_POINT('',(16.5085576038968,35.6304565378295,-25.5));
#125065=CARTESIAN_POINT('Origin',(16.5085576038968,35.1304565378295,-25.5));
#125066=CARTESIAN_POINT('Origin',(16.5085576038968,36.1384565378295,-26.));
#125067=CARTESIAN_POINT('Origin',(16.5085576038968,36.1384565378295,-25.5));
#125068=CARTESIAN_POINT('Origin',(8.25411460523903,35.1304565378295,-25.5));
#125069=CARTESIAN_POINT('',(16.8285576038968,35.1304565378295,-26.));
#125070=CARTESIAN_POINT('',(16.8285576038968,35.6304565378295,-25.5));
#125071=CARTESIAN_POINT('Origin',(16.8285576038968,35.1304565378295,-25.5));
#125072=CARTESIAN_POINT('',(8.25411460523903,35.1304565378295,-26.));
#125073=CARTESIAN_POINT('',(8.25411460523903,35.6304565378295,-25.5));
#125074=CARTESIAN_POINT('Origin',(16.8285576038968,32.6304565378295,-25.5));
#125075=CARTESIAN_POINT('',(18.5963245568632,34.3982234907959,-26.));
#125076=CARTESIAN_POINT('',(18.9498779474565,34.7517768813891,-25.5));
#125077=CARTESIAN_POINT('Origin',(18.5963245568632,34.3982234907959,-25.5));
#125078=CARTESIAN_POINT('Origin',(16.8285576038968,32.6304565378295,-26.));
#125079=CARTESIAN_POINT('Origin',(16.8285576038968,32.6304565378295,-25.5));
#125080=CARTESIAN_POINT('Origin',(15.5139901477705,37.4805578998886,-25.5));
#125081=CARTESIAN_POINT('',(24.1817610214557,28.8127870262033,-26.));
#125082=CARTESIAN_POINT('',(24.535314412049,29.1663404167966,-25.5));
#125083=CARTESIAN_POINT('Origin',(24.1817610214557,28.8127870262033,-25.5));
#125084=CARTESIAN_POINT('',(15.5139901477705,37.4805578998886,-26.));
#125085=CARTESIAN_POINT('',(15.8675435383638,37.8341112904819,-25.5));
#125086=CARTESIAN_POINT('Origin',(20.9997805061163,25.6308065108639,-25.5));
#125087=CARTESIAN_POINT('',(25.4997805061163,25.6308065108639,-26.));
#125088=CARTESIAN_POINT('',(25.9997805061163,25.6308065108639,-25.5));
#125089=CARTESIAN_POINT('Origin',(25.4997805061163,25.6308065108639,-25.5));
#125090=CARTESIAN_POINT('Origin',(20.9997805061163,25.6308065108639,-26.));
#125091=CARTESIAN_POINT('Origin',(20.9997805061163,25.6308065108639,-25.5));
#125092=CARTESIAN_POINT('Origin',(25.4997805061163,26.8808573438743,-25.5));
#125093=CARTESIAN_POINT('',(25.4997805061163,12.1308065108639,-26.));
#125094=CARTESIAN_POINT('',(25.9997805061163,12.1308065108639,-25.5));
#125095=CARTESIAN_POINT('Origin',(25.4997805061163,12.1308065108639,-25.5));
#125096=CARTESIAN_POINT('',(25.4997805061163,26.8808573438743,-26.));
#125097=CARTESIAN_POINT('',(25.9997805061163,26.8808573438743,-25.5));
#125098=CARTESIAN_POINT('Ctrl Pts',(25.9997805061163,12.1308065108638,-25.5));
#125099=CARTESIAN_POINT('Ctrl Pts',(25.9997805061164,11.1308065108638,-25.5));
#125100=CARTESIAN_POINT('Ctrl Pts',(24.9997805061164,11.1308065108639,-25.5));
#125101=CARTESIAN_POINT('Ctrl Pts',(25.9997805061163,12.1308065108638,-26.));
#125102=CARTESIAN_POINT('Ctrl Pts',(25.9997805061164,11.1308065108638,-26.));
#125103=CARTESIAN_POINT('Ctrl Pts',(24.9997805061164,11.1308065108639,-26.));
#125104=CARTESIAN_POINT('Ctrl Pts',(25.4997805061163,12.1308065108638,-26.));
#125105=CARTESIAN_POINT('Ctrl Pts',(25.4997805061163,11.6308065108639,-26.));
#125106=CARTESIAN_POINT('Ctrl Pts',(24.9997805061164,11.630806510864,-26.));
#125107=CARTESIAN_POINT('',(24.9997805061163,11.6308065108639,-26.));
#125108=CARTESIAN_POINT('',(24.9997805061163,11.1308065108639,-25.5));
#125109=CARTESIAN_POINT('Origin',(24.9997805061163,11.6308065108639,-25.5));
#125110=CARTESIAN_POINT('Origin',(24.9997805061163,12.1308065108639,-26.));
#125111=CARTESIAN_POINT('Origin',(24.9997805061163,12.1308065108639,-25.5));
#125112=CARTESIAN_POINT('Origin',(12.4997260563488,11.6308065108639,-25.5));
#125113=CARTESIAN_POINT('',(20.4997805061163,11.1308065108639,-25.5));
#125114=CARTESIAN_POINT('',(12.4997260563488,11.1308065108639,-25.5));
#125115=CARTESIAN_POINT('',(20.7068872873028,11.6308065108639,-26.));
#125116=CARTESIAN_POINT('Origin',(20.7068872873028,11.6308065108639,-25.5));
#125117=CARTESIAN_POINT('',(12.4997260563488,11.6308065108639,-26.));
#125118=CARTESIAN_POINT('Origin',(11.4782812553205,20.8594125428461,-25.5));
#125119=CARTESIAN_POINT('',(19.0000070232196,12.6305799937605,-25.5));
#125120=CARTESIAN_POINT('',(11.1247278647273,20.5058591522529,-25.5));
#125121=CARTESIAN_POINT('',(19.5000070232196,12.8376867749471,-26.));
#125122=CARTESIAN_POINT('Origin',(19.5000070232196,12.8376867749471,-25.5));
#125123=CARTESIAN_POINT('',(11.4782812553205,20.8594125428461,-26.));
#125124=CARTESIAN_POINT('Origin',(19.5000070232196,20.3807440853227,-25.5));
#125125=CARTESIAN_POINT('',(19.5000070232196,21.8015799937605,-26.));
#125126=CARTESIAN_POINT('',(19.5000070232196,20.3807440853227,-26.));
#125127=CARTESIAN_POINT('',(19.0000070232196,21.8015799937605,-25.5));
#125128=CARTESIAN_POINT('',(19.0000070232196,20.3807440853227,-25.5));
#125129=CARTESIAN_POINT('Origin',(19.5000070232196,21.8015799937605,-25.5));
#125130=CARTESIAN_POINT('Origin',(18.0000070232196,21.8015799937605,-25.5));
#125131=CARTESIAN_POINT('',(18.7042143673984,23.1260013830489,-26.));
#125132=CARTESIAN_POINT('',(18.4694785860055,22.6845275866195,-25.5));
#125133=CARTESIAN_POINT('Origin',(18.7042143673984,23.1260013830489,-25.5));
#125134=CARTESIAN_POINT('Origin',(18.0000070232196,21.8015799937605,-26.));
#125135=CARTESIAN_POINT('Origin',(18.0000070232196,21.8015799937605,-25.5));
#125136=CARTESIAN_POINT('Origin',(10.3759028387591,27.5542431726415,-25.5));
#125137=CARTESIAN_POINT('',(15.75,24.1305,-25.5));
#125138=CARTESIAN_POINT('',(10.1411670573662,27.112769376212,-25.5));
#125139=CARTESIAN_POINT('',(15.8746640014216,24.6305,-26.));
#125140=CARTESIAN_POINT('Origin',(15.8746640014216,24.6305,-25.5));
#125141=CARTESIAN_POINT('',(10.3759028387591,27.5542431726415,-26.));
#125142=CARTESIAN_POINT('Origin',(7.87483580329061,24.6305,-25.5));
#125143=CARTESIAN_POINT('',(7.87483580329061,24.6305,-26.));
#125144=CARTESIAN_POINT('',(7.87483580329061,24.1305,-25.5));
#125145=CARTESIAN_POINT('Origin',(-9.01646660547503,28.2774328600768,-25.5));
#125146=CARTESIAN_POINT('',(-18.7044786694047,23.12666906083,-26.));
#125147=CARTESIAN_POINT('',(-9.01646660547503,28.2774328600768,-26.));
#125148=CARTESIAN_POINT('',(-18.4697586471852,22.6851868854601,-25.5));
#125149=CARTESIAN_POINT('',(-8.78174658325559,27.8359506847069,-25.5));
#125150=CARTESIAN_POINT('Origin',(-18.7044786694047,23.12666906083,-25.5));
#125151=CARTESIAN_POINT('Origin',(-18.0003186027463,21.8022225347204,-25.5));
#125152=CARTESIAN_POINT('',(-19.5003186017906,21.8022760793161,-26.));
#125153=CARTESIAN_POINT('',(-19.0003186021092,21.8022582311175,-25.5));
#125154=CARTESIAN_POINT('Origin',(-19.5003186017906,21.8022760793161,-25.5));
#125155=CARTESIAN_POINT('Origin',(-18.0003186027463,21.8022225347204,-26.));
#125156=CARTESIAN_POINT('Origin',(-18.0003186027463,21.8022225347204,-25.5));
#125157=CARTESIAN_POINT('Origin',(-19.5002056346847,24.9669401637651,-25.5));
#125158=CARTESIAN_POINT('',(-19.000645973767,12.6312582369605,-25.5));
#125159=CARTESIAN_POINT('',(-19.0002056350033,24.9669223155665,-25.5));
#125160=CARTESIAN_POINT('',(-19.5006385804826,12.8383828662136,-26.));
#125161=CARTESIAN_POINT('Origin',(-19.5006385804826,12.8383828662136,-25.5));
#125162=CARTESIAN_POINT('',(-19.5002056346847,24.9669401637651,-26.));
#125163=CARTESIAN_POINT('Origin',(-10.7288557519193,21.609539475044,-25.5));
#125164=CARTESIAN_POINT('',(-20.707561925074,11.6315456841765,-26.));
#125165=CARTESIAN_POINT('',(-10.7288557519193,21.609539475044,-26.));
#125166=CARTESIAN_POINT('',(-20.500472992218,11.1315382915292,-25.5));
#125167=CARTESIAN_POINT('',(-10.3753149821335,21.2559734640938,-25.5));
#125168=CARTESIAN_POINT('Origin',(-20.707561925074,11.6315456841765,-25.5));
#125169=CARTESIAN_POINT('Origin',(-10.2506862658096,11.6311724113903,-25.5));
#125170=CARTESIAN_POINT('',(-25.0004551411524,11.6316989249976,-26.));
#125171=CARTESIAN_POINT('',(-10.2506862658096,11.6311724113903,-26.));
#125172=CARTESIAN_POINT('',(-25.0004729893509,11.1316989253161,-25.5));
#125173=CARTESIAN_POINT('',(-10.2507041140081,11.1311724117089,-25.5));
#125174=CARTESIAN_POINT('Origin',(-25.0004551411524,11.6316989249976,-25.5));
#125175=CARTESIAN_POINT('Ctrl Pts',(-25.0004729893509,11.1316989253161,
-25.5));
#125176=CARTESIAN_POINT('Ctrl Pts',(-26.000472988714,11.131734621713,-25.5));
#125177=CARTESIAN_POINT('Ctrl Pts',(-26.0004372923167,12.1317346210762,
-25.5));
#125178=CARTESIAN_POINT('Ctrl Pts',(-25.0004729893508,11.1316989253161,
-26.));
#125179=CARTESIAN_POINT('Ctrl Pts',(-26.000472988714,11.131734621713,-26.0000000000001));
#125180=CARTESIAN_POINT('Ctrl Pts',(-26.0004372923167,12.1317346210762,
-26.));
#125181=CARTESIAN_POINT('Ctrl Pts',(-25.0004551411524,11.6316989249976,
-26.));
#125182=CARTESIAN_POINT('Ctrl Pts',(-25.5004551408338,11.6317167731961,
-26.));
#125183=CARTESIAN_POINT('Ctrl Pts',(-25.5004372926352,12.1317167728775,
-26.));
#125184=CARTESIAN_POINT('',(-25.5004372926353,12.1317167728775,-26.));
#125185=CARTESIAN_POINT('',(-26.0004372923167,12.1317346210761,-25.5));
#125186=CARTESIAN_POINT('Origin',(-25.5004372926353,12.1317167728775,-25.5));
#125187=CARTESIAN_POINT('Origin',(-25.0004372929538,12.131698924679,-26.));
#125188=CARTESIAN_POINT('Origin',(-25.0004372929538,12.131698924679,-25.5));
#125189=CARTESIAN_POINT('Origin',(-25.5001517196441,20.1317675956942,-25.5));
#125190=CARTESIAN_POINT('',(-25.4999553912744,25.6317167642765,-26.));
#125191=CARTESIAN_POINT('',(-25.9999553909559,25.631734612475,-25.5));
#125192=CARTESIAN_POINT('Origin',(-25.4999553912744,25.6317167642765,-25.5));
#125193=CARTESIAN_POINT('',(-25.5001517196441,20.1317675956942,-26.));
#125194=CARTESIAN_POINT('',(-26.0001517193255,20.1317854438928,-25.5));
#125195=CARTESIAN_POINT('Origin',(-20.9999553941414,25.6315561304895,-25.5));
#125196=CARTESIAN_POINT('',(-24.1818223222136,28.8136502290417,-26.));
#125197=CARTESIAN_POINT('',(-24.5353630919994,29.167216239992,-25.5));
#125198=CARTESIAN_POINT('Origin',(-24.1818223222136,28.8136502290417,-25.5));
#125199=CARTESIAN_POINT('Origin',(-20.9999553941414,25.6315561304895,-26.));
#125200=CARTESIAN_POINT('Origin',(-20.9999553941414,25.6315561304895,-25.5));
#125201=CARTESIAN_POINT('Origin',(-18.3067027565145,34.6883503685105,-25.5));
#125202=CARTESIAN_POINT('',(-18.5961864812216,34.3988873101177,-26.));
#125203=CARTESIAN_POINT('',(-18.9497272510074,34.7524533210679,-25.5));
#125204=CARTESIAN_POINT('Origin',(-18.5961864812216,34.3988873101177,-25.5));
#125205=CARTESIAN_POINT('',(-18.3067027565145,34.6883503685105,-26.));
#125206=CARTESIAN_POINT('',(-18.6602435263003,35.0419163794607,-25.5));
#125207=CARTESIAN_POINT('Origin',(-16.8284826322926,32.6310572553665,-25.5));
#125208=CARTESIAN_POINT('',(-16.8283933912999,35.1310572537737,-26.));
#125209=CARTESIAN_POINT('',(-16.8283755431013,35.6310572534551,-25.5));
#125210=CARTESIAN_POINT('Origin',(-16.8283933912999,35.1310572537737,-25.5));
#125211=CARTESIAN_POINT('Origin',(-16.8284826322926,32.6310572553665,-26.));
#125212=CARTESIAN_POINT('Origin',(-16.8284826322926,32.6310572553665,-25.5));
#125213=CARTESIAN_POINT('Origin',(-8.41423596303023,35.1307568986686,-25.5));
#125214=CARTESIAN_POINT('',(-16.5083933915038,35.1310458309266,-26.));
#125215=CARTESIAN_POINT('',(-16.5083755433052,35.631045830608,-25.5));
#125216=CARTESIAN_POINT('Origin',(-16.5083933915038,35.1310458309266,-25.5));
#125217=CARTESIAN_POINT('',(-8.41423596303023,35.1307568986686,-26.));
#125218=CARTESIAN_POINT('',(-8.41421811483168,35.6307568983501,-25.5));
#125219=CARTESIAN_POINT('Origin',(-16.5083574095355,36.1390458302844,-25.5));
#125220=CARTESIAN_POINT('',(-15.5003574101777,36.1390098483161,-26.));
#125221=CARTESIAN_POINT('',(-16.0003574098591,36.1390276965147,-25.5));
#125222=CARTESIAN_POINT('Origin',(-15.5003574101777,36.1390098483161,-25.5));
#125223=CARTESIAN_POINT('Origin',(-16.5083574095355,36.1390458302844,-26.));
#125224=CARTESIAN_POINT('Origin',(-16.5083574095355,36.1390458302844,-25.5));
#125225=CARTESIAN_POINT('Origin',(-15.5005003304909,32.1352356652978,-25.5));
#125226=CARTESIAN_POINT('',(-15.5000542763735,44.6310098429057,-26.));
#125227=CARTESIAN_POINT('',(-16.0000542760549,44.6310276911043,-25.5));
#125228=CARTESIAN_POINT('Origin',(-15.5000542763735,44.6310098429057,-25.5));
#125229=CARTESIAN_POINT('',(-15.5005003304909,32.1352356652978,-26.));
#125230=CARTESIAN_POINT('',(-16.0005003301724,32.1352535134963,-25.5));
#125231=CARTESIAN_POINT('Origin',(6.40011460523903,44.6304565378295,-25.5));
#125232=CARTESIAN_POINT('',(12.8005576038968,45.1304565378295,-25.5));
#125233=CARTESIAN_POINT('',(12.8005576038968,44.6304565378295,-26.));
#125234=CARTESIAN_POINT('Origin',(12.8005576038968,44.6304565378295,-25.5));
#125235=CARTESIAN_POINT('',(15.5005576038968,45.1304565378295,-25.5));
#125236=CARTESIAN_POINT('',(6.40011460523903,45.1304565378295,-25.5));
#125237=CARTESIAN_POINT('Origin',(15.5005576038968,44.6304565378295,-25.5));
#125238=CARTESIAN_POINT('',(6.40011460523903,44.6304565378295,-26.));
#125239=CARTESIAN_POINT('Origin',(-6.40003962806013,44.6307992338217,-25.5));
#125240=CARTESIAN_POINT('',(-12.8000453539944,44.6309134623946,-26.));
#125241=CARTESIAN_POINT('',(-6.40003962806013,44.6307992338217,-26.));
#125242=CARTESIAN_POINT('',(-12.8000364298952,45.130913462315,-25.5));
#125243=CARTESIAN_POINT('Origin',(-12.8000453539944,44.6309134623946,-25.5));
#125244=CARTESIAN_POINT('',(-6.40003070396085,45.130799233742,-25.5));
#125245=CARTESIAN_POINT('Origin',(-7.74989684768079,44.6307331902084,-25.5));
#125246=CARTESIAN_POINT('',(-7.74989684768079,44.6307331902084,-26.));
#125247=CARTESIAN_POINT('',(-15.5000364281749,45.1310098425872,-25.5));
#125248=CARTESIAN_POINT('Origin',(-15.5000542763735,44.6310098429057,-25.5));
#125249=CARTESIAN_POINT('',(-7.74987899948224,45.1307331898898,-25.5));
#125250=CARTESIAN_POINT('Origin',(-15.5000542763735,44.6310098429057,-25.5));
#125251=CARTESIAN_POINT('Origin',(-15.5000542763735,44.6310098429057,-25.5));
#125252=CARTESIAN_POINT('Origin',(15.5005576038968,44.6304565378295,-25.5));
#125253=CARTESIAN_POINT('Origin',(15.5005576038968,44.6304565378295,-25.5));
#125254=CARTESIAN_POINT('Origin',(-15.7502284469069,24.1310622223319,-26.));
#125255=CARTESIAN_POINT('',(-15.7502284469069,24.1310622223319,-12.5));
#125256=CARTESIAN_POINT('',(-15.7502284469069,24.1310622223319,-26.));
#125257=CARTESIAN_POINT('',(-18.4697586471852,22.6851868854601,-12.5));
#125258=CARTESIAN_POINT('',(-8.78174658325559,27.8359506847069,-12.5));
#125259=CARTESIAN_POINT('',(-18.4697586471852,22.6851868854601,-26.));
#125260=CARTESIAN_POINT('Origin',(-18.0003186027463,21.8022225347204,-26.));
#125261=CARTESIAN_POINT('',(-19.0003186021092,21.8022582311175,-12.5));
#125262=CARTESIAN_POINT('Origin',(-18.0003186027463,21.8022225347204,-12.5));
#125263=CARTESIAN_POINT('',(-19.0003186021092,21.8022582311175,-26.));
#125264=CARTESIAN_POINT('Origin',(-19.0003186021092,21.8022582311175,-26.));
#125265=CARTESIAN_POINT('',(-19.000645973767,12.6312582369605,-12.5));
#125266=CARTESIAN_POINT('',(-19.0002056350033,24.9669223155665,-12.5));
#125267=CARTESIAN_POINT('',(-19.000645973767,12.6312582369605,-26.));
#125268=CARTESIAN_POINT('Origin',(-19.000645973767,12.6312582369605,-26.));
#125269=CARTESIAN_POINT('',(-20.500472992218,11.1315382915292,-12.5));
#125270=CARTESIAN_POINT('',(-10.3753149821335,21.2559734640938,-12.5));
#125271=CARTESIAN_POINT('',(-20.500472992218,11.1315382915292,-26.));
#125272=CARTESIAN_POINT('Origin',(-20.500472992218,11.1315382915292,-26.));
#125273=CARTESIAN_POINT('',(-25.0004729893509,11.1316989253161,-12.5));
#125274=CARTESIAN_POINT('',(-10.2507041140081,11.1311724117089,-12.5));
#125275=CARTESIAN_POINT('',(-25.0004729893509,11.1316989253161,-26.));
#125276=CARTESIAN_POINT('Origin',(-25.0004372929538,12.131698924679,-26.));
#125277=CARTESIAN_POINT('',(-26.0004372923167,12.1317346210761,-12.5));
#125278=CARTESIAN_POINT('Origin',(-25.0004372929538,12.131698924679,-12.5));
#125279=CARTESIAN_POINT('',(-26.0004372923167,12.1317346210761,-26.));
#125280=CARTESIAN_POINT('Origin',(-26.0004372923167,12.1317346210761,-26.));
#125281=CARTESIAN_POINT('',(-25.9999553909559,25.631734612475,-12.5));
#125282=CARTESIAN_POINT('',(-26.0001517193255,20.1317854438928,-12.5));
#125283=CARTESIAN_POINT('',(-25.9999553909559,25.631734612475,-26.));
#125284=CARTESIAN_POINT('Origin',(-20.9999553941414,25.6315561304895,-26.));
#125285=CARTESIAN_POINT('',(-24.5353630919994,29.167216239992,-12.5));
#125286=CARTESIAN_POINT('Origin',(-20.9999553941414,25.6315561304895,-12.5));
#125287=CARTESIAN_POINT('',(-24.5353630919994,29.167216239992,-26.));
#125288=CARTESIAN_POINT('Origin',(-24.5353630919994,29.167216239992,-26.));
#125289=CARTESIAN_POINT('',(-18.9497272510074,34.7524533210679,-12.5));
#125290=CARTESIAN_POINT('',(-18.6602435263003,35.0419163794607,-12.5));
#125291=CARTESIAN_POINT('',(-18.9497272510074,34.7524533210679,-26.));
#125292=CARTESIAN_POINT('Origin',(-16.8284826322926,32.6310572553665,-26.));
#125293=CARTESIAN_POINT('',(-18.7486119524321,34.9360742604969,-12.5));
#125294=CARTESIAN_POINT('Origin',(-16.8284826322926,32.6310572553665,-12.5));
#125295=CARTESIAN_POINT('',(-18.7486119524321,34.9360742604969,-15.));
#125296=CARTESIAN_POINT('',(-18.7486119524321,34.9360742604969,-12.));
#125297=CARTESIAN_POINT('',(-16.8283755431013,35.6310572534551,-15.));
#125298=CARTESIAN_POINT('Origin',(-16.8284826322926,32.6310572553665,-15.));
#125299=CARTESIAN_POINT('',(-16.8283755431013,35.6310572534551,-26.));
#125300=CARTESIAN_POINT('Origin',(-16.8283755431013,35.6310572534551,-26.));
#125301=CARTESIAN_POINT('',(-16.5083755433052,35.631045830608,-15.));
#125302=CARTESIAN_POINT('',(-16.3514391790885,35.6310402285453,-15.));
#125303=CARTESIAN_POINT('',(-16.5083755433052,35.631045830608,-26.));
#125304=CARTESIAN_POINT('Origin',(-16.5083574095355,36.1390458302844,-26.));
#125305=CARTESIAN_POINT('',(-16.0003574098591,36.1390276965147,-15.));
#125306=CARTESIAN_POINT('Origin',(-16.5083574095355,36.1390458302844,-15.));
#125307=CARTESIAN_POINT('',(-16.0003574098591,36.1390276965147,-26.));
#125308=CARTESIAN_POINT('Origin',(-16.0003574098591,36.1390276965147,-26.));
#125309=CARTESIAN_POINT('',(-16.0002503206678,39.1390276946033,-15.));
#125310=CARTESIAN_POINT('',(-16.0003574097789,36.1390299426383,-15.));
#125311=CARTESIAN_POINT('',(-16.0002503206678,39.1390276946033,-12.5));
#125312=CARTESIAN_POINT('',(-16.0002503206678,39.1390276946033,-12.));
#125313=CARTESIAN_POINT('',(-16.0000542760549,44.6310276911043,-12.5));
#125314=CARTESIAN_POINT('',(-16.0005003301724,32.1352535134963,-12.5));
#125315=CARTESIAN_POINT('',(-16.0000542760549,44.6310276911043,-26.));
#125316=CARTESIAN_POINT('Origin',(-15.5000542763735,44.6310098429057,-26.));
#125317=CARTESIAN_POINT('',(-15.5000364281749,45.1310098425872,-12.5));
#125318=CARTESIAN_POINT('Origin',(-15.5000542763735,44.6310098429057,-12.5));
#125319=CARTESIAN_POINT('',(-15.5000364281749,45.1310098425872,-26.));
#125320=CARTESIAN_POINT('Origin',(-15.5000364281749,45.1310098425872,-26.));
#125321=CARTESIAN_POINT('',(-12.8000364298952,45.130913462315,-12.5));
#125322=CARTESIAN_POINT('',(-7.74987899948224,45.1307331898898,-12.5));
#125323=CARTESIAN_POINT('',(-12.8000364298952,45.130913462315,-26.));
#125324=CARTESIAN_POINT('Origin',(-12.8000364298952,45.130913462315,-26.));
#125325=CARTESIAN_POINT('',(12.8005576038968,45.1304565378295,-12.5));
#125326=CARTESIAN_POINT('',(-6.40003070396085,45.130799233742,-12.5));
#125327=CARTESIAN_POINT('',(12.8005576038968,45.1304565378295,-26.));
#125328=CARTESIAN_POINT('Origin',(12.8005576038968,45.1304565378295,-26.));
#125329=CARTESIAN_POINT('',(15.5005576038968,45.1304565378295,-12.5));
#125330=CARTESIAN_POINT('',(6.40011460523903,45.1304565378295,-12.5));
#125331=CARTESIAN_POINT('',(15.5005576038968,45.1304565378295,-26.));
#125332=CARTESIAN_POINT('Origin',(-0.000328393418778106,28.1309081768848,
-26.));
#125333=CARTESIAN_POINT('Origin',(-15.5005003304909,32.1352356652978,-12.5));
#125334=CARTESIAN_POINT('',(-15.5002337542308,39.6031114612468,-12.));
#125335=CARTESIAN_POINT('Ctrl Pts',(-15.5002337542308,39.6031114612469,
-12.));
#125336=CARTESIAN_POINT('Ctrl Pts',(-15.5012802807782,39.6022052080442,
-12.));
#125337=CARTESIAN_POINT('Ctrl Pts',(-15.5023266329781,39.6012987501675,
-12.0000032854501));
#125338=CARTESIAN_POINT('Ctrl Pts',(-15.5262620426631,39.580555287795,-12.0001535475902));
#125339=CARTESIAN_POINT('Ctrl Pts',(-15.549079071856,39.5606097425883,-12.0018685097915));
#125340=CARTESIAN_POINT('Ctrl Pts',(-15.6555915595815,39.4666813170044,
-12.0172417791965));
#125341=CARTESIAN_POINT('Ctrl Pts',(-15.7342867260662,39.3947272458287,
-12.0503680939609));
#125342=CARTESIAN_POINT('Ctrl Pts',(-15.8544463319837,39.2818437637677,
-12.1407858340455));
#125343=CARTESIAN_POINT('Ctrl Pts',(-15.8992348499764,39.2385644267119,
-12.1913094880828));
#125344=CARTESIAN_POINT('Ctrl Pts',(-15.9582815856617,39.1808059783461,
-12.2931553699351));
#125345=CARTESIAN_POINT('Ctrl Pts',(-15.9780823063818,39.1611342110301,
-12.3427321807669));
#125346=CARTESIAN_POINT('Ctrl Pts',(-15.996608615715,39.1426753037105,-12.4305871755405));
#125347=CARTESIAN_POINT('Ctrl Pts',(-16.0002503206678,39.1390276946034,
-12.4651445835938));
#125348=CARTESIAN_POINT('Ctrl Pts',(-16.0002503206678,39.1390276946034,
-12.5));
#125349=CARTESIAN_POINT('',(-15.5000542763735,44.6310098429057,-12.));
#125350=CARTESIAN_POINT('',(-15.5005003304909,32.1352356652978,-12.));
#125351=CARTESIAN_POINT('Origin',(-15.5000542763735,44.6310098429057,-12.5));
#125352=CARTESIAN_POINT('Origin',(-16.0003574098591,36.1390276965147,-12.5));
#125353=CARTESIAN_POINT('',(-18.8658210632966,34.1292719773217,-12.));
#125354=CARTESIAN_POINT('Origin',(-16.0003574098591,36.1390276965147,-12.));
#125355=CARTESIAN_POINT('Origin',(-16.0003574098591,36.1390276965147,-12.5));
#125356=CARTESIAN_POINT('',(-18.810086036752,34.6128021370802,-12.1018952060707));
#125357=CARTESIAN_POINT('Ctrl Pts',(-18.810086036752,34.6128021370802,-12.1018952060707));
#125358=CARTESIAN_POINT('Ctrl Pts',(-18.8089992232141,34.6203016604522,
-12.1053410081124));
#125359=CARTESIAN_POINT('Ctrl Pts',(-18.8078973392296,34.6277440210717,
-12.1088851897267));
#125360=CARTESIAN_POINT('Ctrl Pts',(-18.7957307106799,34.7082643255815,
-12.1486504715915));
#125361=CARTESIAN_POINT('Ctrl Pts',(-18.784159852527,34.7702166242448,-12.1921413513201));
#125362=CARTESIAN_POINT('Ctrl Pts',(-18.7672884639414,34.8535445163286,
-12.2764946297254));
#125363=CARTESIAN_POINT('Ctrl Pts',(-18.7606689443804,34.8835886882299,
-12.3169287768681));
#125364=CARTESIAN_POINT('Ctrl Pts',(-18.7520329511296,34.9216311139679,
-12.3986190308673));
#125365=CARTESIAN_POINT('Ctrl Pts',(-18.7494922500063,34.9323419849364,
-12.4373510176214));
#125366=CARTESIAN_POINT('Ctrl Pts',(-18.7486753311664,34.9358059214554,
-12.4851148185871));
#125367=CARTESIAN_POINT('Ctrl Pts',(-18.7486119524321,34.936074260497,-12.4925693313125));
#125368=CARTESIAN_POINT('Ctrl Pts',(-18.7486119524321,34.936074260497,-12.5));
#125369=CARTESIAN_POINT('Ctrl Pts',(-18.8658210632966,34.1292719773218,
-12.));
#125370=CARTESIAN_POINT('Ctrl Pts',(-18.8656807480304,34.1308827000775,
-12.));
#125371=CARTESIAN_POINT('Ctrl Pts',(-18.8655400049988,34.1324933903514,
-12.0000032434225));
#125372=CARTESIAN_POINT('Ctrl Pts',(-18.8573778375601,34.2256175041334,
-12.0003779495169));
#125373=CARTESIAN_POINT('Ctrl Pts',(-18.8478563981533,34.3178692956096,
-12.0111952320962));
#125374=CARTESIAN_POINT('Ctrl Pts',(-18.8288764025859,34.4771426650498,
-12.048491997422));
#125375=CARTESIAN_POINT('Ctrl Pts',(-18.8196146553393,34.5470501977567,
-12.0716841972469));
#125376=CARTESIAN_POINT('Ctrl Pts',(-18.810086036752,34.6128021370802,-12.1018952060707));
#125377=CARTESIAN_POINT('Origin',(-7.74989684768079,44.6307331902083,-12.5));
#125378=CARTESIAN_POINT('',(-12.8000542780937,44.6309134626335,-12.));
#125379=CARTESIAN_POINT('Origin',(-12.8000542780937,44.6309134626335,-12.5));
#125380=CARTESIAN_POINT('Origin',(-15.5000542763735,44.6310098429057,-12.5));
#125381=CARTESIAN_POINT('',(-7.74989684768079,44.6307331902083,-12.));
#125382=CARTESIAN_POINT('Origin',(-6.40003962806013,44.6307992338217,-12.5));
#125383=CARTESIAN_POINT('',(12.8005486797976,44.6304565379091,-12.));
#125384=CARTESIAN_POINT('Origin',(12.8005486797976,44.6304565379091,-12.5));
#125385=CARTESIAN_POINT('',(-6.40003962806013,44.6307992338217,-12.));
#125386=CARTESIAN_POINT('Origin',(6.40011460523903,44.6304565378295,-12.5));
#125387=CARTESIAN_POINT('',(15.5005576038968,44.6304565378295,-12.));
#125388=CARTESIAN_POINT('',(6.40011460523903,44.6304565378295,-12.));
#125389=CARTESIAN_POINT('Origin',(15.5005576038968,44.6304565378295,-12.5));
#125390=CARTESIAN_POINT('Origin',(-15.5000542763735,44.6310098429057,-12.5));
#125391=CARTESIAN_POINT('Origin',(16.0005576038968,36.1384565378295,-12.5));
#125392=CARTESIAN_POINT('',(16.0005576038968,39.1384565378295,-12.5));
#125393=CARTESIAN_POINT('',(18.7487692036153,34.9354049997927,-12.5));
#125394=CARTESIAN_POINT('Origin',(16.0005576038968,36.1384565378295,-12.5));
#125395=CARTESIAN_POINT('',(15.5005576038968,39.6025581529673,-12.));
#125396=CARTESIAN_POINT('Ctrl Pts',(15.5005576038968,39.6025581529673,-12.));
#125397=CARTESIAN_POINT('Ctrl Pts',(15.5016040980935,39.601651862408,-12.));
#125398=CARTESIAN_POINT('Ctrl Pts',(15.5026504179355,39.6007453671807,-12.0000032854501));
#125399=CARTESIAN_POINT('Ctrl Pts',(15.5265850871382,39.5800010504138,-12.0001535475902));
#125400=CARTESIAN_POINT('Ctrl Pts',(15.5494014043324,39.5600546907341,-12.0018685097915));
#125401=CARTESIAN_POINT('Ctrl Pts',(15.6559105390839,39.4661224630978,-12.0172417791965));
#125402=CARTESIAN_POINT('Ctrl Pts',(15.7346031370173,39.394165582834,-12.0503680939609));
#125403=CARTESIAN_POINT('Ctrl Pts',(15.8547587133249,39.2812778115798,-12.1407858340455));
#125404=CARTESIAN_POINT('Ctrl Pts',(15.8995456863726,39.2379968757629,-12.1913094880829));
#125405=CARTESIAN_POINT('Ctrl Pts',(15.9585903602516,39.1802363196783,-12.2931553699351));
#125406=CARTESIAN_POINT('Ctrl Pts',(15.9783903787479,39.1605638455604,-12.3427321807669));
#125407=CARTESIAN_POINT('Ctrl Pts',(15.9969160291529,39.1421042769301,-12.4305871755405));
#125408=CARTESIAN_POINT('Ctrl Pts',(16.0005576038968,39.1384565378295,-12.4651445835938));
#125409=CARTESIAN_POINT('Ctrl Pts',(16.0005576038968,39.1384565378295,-12.5));
#125410=CARTESIAN_POINT('',(18.8659495144705,34.1285985331886,-12.));
#125411=CARTESIAN_POINT('Origin',(16.0005576038968,36.1384565378295,-12.));
#125412=CARTESIAN_POINT('',(18.8102317482459,34.6121306821786,-12.1018952060707));
#125413=CARTESIAN_POINT('Ctrl Pts',(18.8102317482459,34.6121306821786,-12.1018952060707));
#125414=CARTESIAN_POINT('Ctrl Pts',(18.8197580197198,34.5463784027596,-12.0716841972469));
#125415=CARTESIAN_POINT('Ctrl Pts',(18.8290172715136,34.4764705394863,-12.048491997422));
#125416=CARTESIAN_POINT('Ctrl Pts',(18.8479915815835,34.3171964926297,-12.0111952320961));
#125417=CARTESIAN_POINT('Ctrl Pts',(18.8575097279277,34.2249443613295,-12.0003779495169));
#125418=CARTESIAN_POINT('Ctrl Pts',(18.8656685711657,34.131819956249,-12.0000032434225));
#125419=CARTESIAN_POINT('Ctrl Pts',(18.8658092567013,34.130209260952,-12.));
#125420=CARTESIAN_POINT('Ctrl Pts',(18.8659495144705,34.1285985331886,-12.));
#125421=CARTESIAN_POINT('Ctrl Pts',(18.7487692036153,34.9354049997927,-12.5));
#125422=CARTESIAN_POINT('Ctrl Pts',(18.7487692036153,34.9354049997927,-12.4925693313125));
#125423=CARTESIAN_POINT('Ctrl Pts',(18.7488325727708,34.9351366584889,-12.4851148185871));
#125424=CARTESIAN_POINT('Ctrl Pts',(18.7496493679601,34.9316726928111,-12.4373510176214));
#125425=CARTESIAN_POINT('Ctrl Pts',(18.7521896867423,34.9209617311555,-12.3986190308672));
#125426=CARTESIAN_POINT('Ctrl Pts',(18.7608243220101,34.8829189971679,-12.3169287768681));
#125427=CARTESIAN_POINT('Ctrl Pts',(18.7674427690982,34.8528745889928,-12.2764946297254));
#125428=CARTESIAN_POINT('Ctrl Pts',(18.7843111831676,34.769546094714,-12.1921413513198));
#125429=CARTESIAN_POINT('Ctrl Pts',(18.7958798298392,34.7075933830521,-12.1486504715914));
#125430=CARTESIAN_POINT('Ctrl Pts',(18.8080435840964,34.6270726442891,-12.1088851897267));
#125431=CARTESIAN_POINT('Ctrl Pts',(18.8091452024147,34.6196302443412,-12.1053410081124));
#125432=CARTESIAN_POINT('Ctrl Pts',(18.8102317482459,34.6121306821786,-12.1018952060707));
#125433=CARTESIAN_POINT('Origin',(15.5005576038968,36.3806823573572,-12.5));
#125434=CARTESIAN_POINT('',(15.5005576038968,36.3806823573572,-12.));
#125435=CARTESIAN_POINT('',(16.0005576038968,44.6304565378295,-12.5));
#125436=CARTESIAN_POINT('',(16.0005576038968,36.3806823573572,-12.5));
#125437=CARTESIAN_POINT('Origin',(15.5005576038968,44.6304565378295,-12.5));
#125438=CARTESIAN_POINT('Origin',(15.5005576038968,44.6304565378295,-12.5));
#125439=CARTESIAN_POINT('Origin',(15.5005576038968,44.6304565378295,-12.5));
#125440=CARTESIAN_POINT('Origin',(-18.3067027565145,34.6883503685105,-12.5));
#125441=CARTESIAN_POINT('Origin',(-18.5961864812216,34.3988873101177,-12.5));
#125442=CARTESIAN_POINT('',(-24.1818223222136,28.8136502290417,-12.));
#125443=CARTESIAN_POINT('Origin',(-24.1818223222136,28.8136502290417,-12.5));
#125444=CARTESIAN_POINT('',(-18.3067027565145,34.6883503685105,-12.));
#125445=CARTESIAN_POINT('Origin',(-0.000328393418778106,28.1309081768848,
-12.));
#125446=CARTESIAN_POINT('',(-25.4999553912744,25.6317167642765,-12.));
#125447=CARTESIAN_POINT('Origin',(-20.9999553941414,25.6315561304895,-12.));
#125448=CARTESIAN_POINT('',(-25.5004372926353,12.1317167728775,-12.));
#125449=CARTESIAN_POINT('',(-25.5001517196441,20.1317675956942,-12.));
#125450=CARTESIAN_POINT('',(-25.0004551411524,11.6316989249976,-12.));
#125451=CARTESIAN_POINT('Origin',(-25.0004372929538,12.131698924679,-12.));
#125452=CARTESIAN_POINT('',(-20.707561925074,11.6315456841765,-12.));
#125453=CARTESIAN_POINT('',(-10.2506862658096,11.6311724113903,-12.));
#125454=CARTESIAN_POINT('',(-19.5006385804826,12.8383828662136,-12.));
#125455=CARTESIAN_POINT('',(-10.7288557519193,21.609539475044,-12.));
#125456=CARTESIAN_POINT('',(-19.5003186017906,21.8022760793161,-12.));
#125457=CARTESIAN_POINT('',(-19.5002056346847,24.9669401637651,-12.));
#125458=CARTESIAN_POINT('',(-18.7044786694047,23.12666906083,-12.));
#125459=CARTESIAN_POINT('Origin',(-18.0003186027463,21.8022225347204,-12.));
#125460=CARTESIAN_POINT('',(-15.8748746000505,24.631066672069,-12.));
#125461=CARTESIAN_POINT('',(-9.01646660547503,28.2774328600768,-12.));
#125462=CARTESIAN_POINT('',(-12.0002195251968,24.6309283607631,-12.));
#125463=CARTESIAN_POINT('',(-6.00033197323811,24.630714186474,-12.));
#125464=CARTESIAN_POINT('',(12.,24.6305,-12.));
#125465=CARTESIAN_POINT('',(5.99980902926158,24.6306070926795,-12.));
#125466=CARTESIAN_POINT('',(15.8746640014216,24.6305,-12.));
#125467=CARTESIAN_POINT('',(7.87483580329061,24.6305,-12.));
#125468=CARTESIAN_POINT('',(18.7042143673984,23.1260013830489,-12.));
#125469=CARTESIAN_POINT('',(10.3759028387591,27.5542431726415,-12.));
#125470=CARTESIAN_POINT('',(19.5000070232196,21.8015799937605,-12.));
#125471=CARTESIAN_POINT('Origin',(18.0000070232196,21.8015799937605,-12.));
#125472=CARTESIAN_POINT('',(19.5000070232196,12.8376867749471,-12.));
#125473=CARTESIAN_POINT('',(19.5000070232196,20.3807440853227,-12.));
#125474=CARTESIAN_POINT('',(20.7068872873028,11.6308065108639,-12.));
#125475=CARTESIAN_POINT('',(11.4782812553205,20.8594125428461,-12.));
#125476=CARTESIAN_POINT('',(24.9997805061163,11.6308065108639,-12.));
#125477=CARTESIAN_POINT('',(12.4997260563488,11.6308065108639,-12.));
#125478=CARTESIAN_POINT('',(25.4997805061163,12.1308065108639,-12.));
#125479=CARTESIAN_POINT('Origin',(24.9997805061163,12.1308065108639,-12.));
#125480=CARTESIAN_POINT('',(25.4997805061163,25.6308065108639,-12.));
#125481=CARTESIAN_POINT('',(25.4997805061163,26.8808573438743,-12.));
#125482=CARTESIAN_POINT('',(24.1817610214557,28.8127870262033,-12.));
#125483=CARTESIAN_POINT('Origin',(20.9997805061163,25.6308065108639,-12.));
#125484=CARTESIAN_POINT('',(15.5139901477705,37.4805578998886,-12.));
#125485=CARTESIAN_POINT('Origin',(15.5139901477705,37.4805578998886,-12.5));
#125486=CARTESIAN_POINT('',(24.535314412049,29.1663404167966,-12.5));
#125487=CARTESIAN_POINT('Origin',(24.1817610214557,28.8127870262033,-12.5));
#125488=CARTESIAN_POINT('',(18.9498779474565,34.7517768813891,-12.5));
#125489=CARTESIAN_POINT('',(15.8675435383638,37.8341112904819,-12.5));
#125490=CARTESIAN_POINT('Origin',(18.5963245568632,34.3982234907959,-12.5));
#125491=CARTESIAN_POINT('Origin',(16.8285576038968,32.6304565378295,-12.5));
#125492=CARTESIAN_POINT('Origin',(16.8285576038968,32.6304565378295,-12.5));
#125493=CARTESIAN_POINT('Origin',(-10.2506862658096,11.6311724113903,-12.5));
#125494=CARTESIAN_POINT('Origin',(-20.707561925074,11.6315456841765,-12.5));
#125495=CARTESIAN_POINT('Origin',(-25.0004551411524,11.6316989249976,-12.5));
#125496=CARTESIAN_POINT('Ctrl Pts',(-25.0004551411523,11.6316989249976,
-12.));
#125497=CARTESIAN_POINT('Ctrl Pts',(-25.5004551408337,11.6317167731962,
-12.));
#125498=CARTESIAN_POINT('Ctrl Pts',(-25.5004372926352,12.1317167728776,
-12.));
#125499=CARTESIAN_POINT('Ctrl Pts',(-25.0004729893509,11.131698925316,-11.9999999999999));
#125500=CARTESIAN_POINT('Ctrl Pts',(-26.0004729887137,11.1317346217132,
-12.));
#125501=CARTESIAN_POINT('Ctrl Pts',(-26.0004372923168,12.131734621076,-11.9999999999999));
#125502=CARTESIAN_POINT('Ctrl Pts',(-25.0004729893509,11.1316989253161,
-12.5000000000001));
#125503=CARTESIAN_POINT('Ctrl Pts',(-26.0004729887137,11.1317346217133,
-12.5000000000001));
#125504=CARTESIAN_POINT('Ctrl Pts',(-26.0004372923167,12.1317346210761,
-12.5));
#125505=CARTESIAN_POINT('Origin',(-25.5004372926353,12.1317167728775,-12.5));
#125506=CARTESIAN_POINT('Origin',(-25.5001517196441,20.1317675956942,-12.5));
#125507=CARTESIAN_POINT('Origin',(-25.4999553912744,25.6317167642765,-12.5));
#125508=CARTESIAN_POINT('Origin',(-20.9999553941414,25.6315561304895,-12.5));
#125509=CARTESIAN_POINT('Origin',(-16.8284826322926,32.6310572553665,-12.5));
#125510=CARTESIAN_POINT('Origin',(-10.7288557519193,21.609539475044,-12.5));
#125511=CARTESIAN_POINT('Origin',(-19.5006385804826,12.8383828662136,-12.5));
#125512=CARTESIAN_POINT('Origin',(-9.01646660547503,28.2774328600768,-12.5));
#125513=CARTESIAN_POINT('Origin',(-15.8748746000505,24.631066672069,-12.5));
#125514=CARTESIAN_POINT('Origin',(-18.7044786694047,23.12666906083,-12.5));
#125515=CARTESIAN_POINT('Origin',(-18.0003186027463,21.8022225347204,-12.5));
#125516=CARTESIAN_POINT('Origin',(-19.5003186017906,21.8022760793161,-12.5));
#125517=CARTESIAN_POINT('Origin',(-19.5002056346847,24.9669401637651,-12.5));
#125518=CARTESIAN_POINT('Origin',(7.87483580329061,24.6305,-12.5));
#125519=CARTESIAN_POINT('',(15.75,24.1305,-12.5));
#125520=CARTESIAN_POINT('',(12.,24.1305,-12.5));
#125521=CARTESIAN_POINT('',(7.87483580329061,24.1305,-12.5));
#125522=CARTESIAN_POINT('Origin',(15.8746640014216,24.6305,-12.5));
#125523=CARTESIAN_POINT('Origin',(12.,24.6305,-12.5));
#125524=CARTESIAN_POINT('Origin',(5.99980902926158,24.6306070926795,-12.5));
#125525=CARTESIAN_POINT('',(-12.0002284492961,24.1309283608428,-12.5));
#125526=CARTESIAN_POINT('Origin',(-12.0002195251968,24.6309283607631,-12.5));
#125527=CARTESIAN_POINT('',(5.9998001051623,24.1306070927591,-12.5));
#125528=CARTESIAN_POINT('Origin',(-6.00033197323811,24.630714186474,-12.5));
#125529=CARTESIAN_POINT('',(-6.00034982143666,24.1307141867926,-12.5));
#125530=CARTESIAN_POINT('Origin',(19.5000070232196,20.3807440853227,-12.5));
#125531=CARTESIAN_POINT('',(19.0000070232196,12.6305799937605,-12.5));
#125532=CARTESIAN_POINT('',(19.0000070232196,21.8015799937605,-12.5));
#125533=CARTESIAN_POINT('',(19.0000070232196,20.3807440853227,-12.5));
#125534=CARTESIAN_POINT('Origin',(19.5000070232196,12.8376867749471,-12.5));
#125535=CARTESIAN_POINT('Origin',(19.5000070232196,21.8015799937605,-12.5));
#125536=CARTESIAN_POINT('Origin',(18.0000070232196,21.8015799937605,-12.5));
#125537=CARTESIAN_POINT('',(18.4694785860055,22.6845275866195,-12.5));
#125538=CARTESIAN_POINT('Origin',(18.7042143673984,23.1260013830489,-12.5));
#125539=CARTESIAN_POINT('Origin',(18.0000070232196,21.8015799937605,-12.5));
#125540=CARTESIAN_POINT('Origin',(10.3759028387591,27.5542431726415,-12.5));
#125541=CARTESIAN_POINT('',(10.1411670573662,27.112769376212,-12.5));
#125542=CARTESIAN_POINT('Origin',(11.4782812553205,20.8594125428461,-12.5));
#125543=CARTESIAN_POINT('',(20.4997805061163,11.1308065108639,-12.5));
#125544=CARTESIAN_POINT('',(11.1247278647273,20.5058591522529,-12.5));
#125545=CARTESIAN_POINT('Origin',(20.7068872873028,11.6308065108639,-12.5));
#125546=CARTESIAN_POINT('Origin',(20.9997805061163,25.6308065108639,-12.5));
#125547=CARTESIAN_POINT('',(25.9997805061163,25.6308065108639,-12.5));
#125548=CARTESIAN_POINT('Origin',(25.4997805061163,25.6308065108639,-12.5));
#125549=CARTESIAN_POINT('Origin',(20.9997805061163,25.6308065108639,-12.5));
#125550=CARTESIAN_POINT('Origin',(25.4997805061163,26.8808573438743,-12.5));
#125551=CARTESIAN_POINT('',(25.9997805061163,12.1308065108639,-12.5));
#125552=CARTESIAN_POINT('Origin',(25.4997805061163,12.1308065108639,-12.5));
#125553=CARTESIAN_POINT('',(25.9997805061163,26.8808573438743,-12.5));
#125554=CARTESIAN_POINT('Ctrl Pts',(25.4997805061163,12.1308065108639,-12.));
#125555=CARTESIAN_POINT('Ctrl Pts',(25.4997805061163,11.6308065108639,-12.));
#125556=CARTESIAN_POINT('Ctrl Pts',(24.9997805061163,11.6308065108639,-12.));
#125557=CARTESIAN_POINT('Ctrl Pts',(25.9997805061163,12.1308065108639,-12.));
#125558=CARTESIAN_POINT('Ctrl Pts',(25.9997805061163,11.1308065108639,-12.));
#125559=CARTESIAN_POINT('Ctrl Pts',(24.9997805061163,11.1308065108639,-12.));
#125560=CARTESIAN_POINT('Ctrl Pts',(25.9997805061163,12.1308065108639,-12.5));
#125561=CARTESIAN_POINT('Ctrl Pts',(25.9997805061163,11.1308065108639,-12.5));
#125562=CARTESIAN_POINT('Ctrl Pts',(24.9997805061163,11.1308065108639,-12.5));
#125563=CARTESIAN_POINT('',(24.9997805061163,11.1308065108639,-12.5));
#125564=CARTESIAN_POINT('Origin',(24.9997805061163,11.6308065108639,-12.5));
#125565=CARTESIAN_POINT('Origin',(24.9997805061163,12.1308065108639,-12.5));
#125566=CARTESIAN_POINT('Origin',(12.4997260563488,11.6308065108639,-12.5));
#125567=CARTESIAN_POINT('',(12.4997260563488,11.1308065108639,-12.5));
#125568=CARTESIAN_POINT('Origin',(-12.0002284492961,24.1309283608428,-26.));
#125569=CARTESIAN_POINT('',(-12.0002284492961,24.1309283608428,-26.));
#125570=CARTESIAN_POINT('Origin',(12.,24.1305,-26.));
#125571=CARTESIAN_POINT('',(12.,24.1305,-26.));
#125572=CARTESIAN_POINT('Origin',(15.75,24.1305,-26.));
#125573=CARTESIAN_POINT('',(15.75,24.1305,-26.));
#125574=CARTESIAN_POINT('Origin',(18.4694785860055,22.6845275866195,-26.));
#125575=CARTESIAN_POINT('',(18.4694785860055,22.6845275866195,-26.));
#125576=CARTESIAN_POINT('Origin',(18.0000070232196,21.8015799937605,-26.));
#125577=CARTESIAN_POINT('',(19.0000070232196,21.8015799937605,-26.));
#125578=CARTESIAN_POINT('Origin',(19.0000070232196,12.6305799937605,-26.));
#125579=CARTESIAN_POINT('',(19.0000070232196,12.6305799937605,-26.));
#125580=CARTESIAN_POINT('Origin',(20.4997805061163,11.1308065108639,-26.));
#125581=CARTESIAN_POINT('',(20.4997805061163,11.1308065108639,-26.));
#125582=CARTESIAN_POINT('Origin',(24.9997805061163,11.1308065108639,-26.));
#125583=CARTESIAN_POINT('',(24.9997805061163,11.1308065108639,-26.));
#125584=CARTESIAN_POINT('Origin',(24.9997805061163,12.1308065108639,-26.));
#125585=CARTESIAN_POINT('',(25.9997805061163,12.1308065108639,-26.));
#125586=CARTESIAN_POINT('Origin',(25.9997805061163,25.6308065108639,-26.));
#125587=CARTESIAN_POINT('',(25.9997805061163,25.6308065108639,-26.));
#125588=CARTESIAN_POINT('Origin',(20.9997805061163,25.6308065108639,-26.));
#125589=CARTESIAN_POINT('',(24.535314412049,29.1663404167966,-26.));
#125590=CARTESIAN_POINT('Origin',(18.9498779474565,34.7517768813891,-26.));
#125591=CARTESIAN_POINT('',(18.9498779474565,34.7517768813891,-26.));
#125592=CARTESIAN_POINT('Origin',(16.8285576038968,32.6304565378295,-26.));
#125593=CARTESIAN_POINT('',(16.8285576038968,35.6304565378295,-15.));
#125594=CARTESIAN_POINT('',(16.8285576038968,35.6304565378295,-26.));
#125595=CARTESIAN_POINT('',(18.7487692036153,34.9354049997927,-15.));
#125596=CARTESIAN_POINT('Origin',(16.8285576038968,32.6304565378295,-15.));
#125597=CARTESIAN_POINT('',(18.7487692036153,34.9354049997927,-12.));
#125598=CARTESIAN_POINT('Origin',(16.0005576038968,36.1384565378295,-12.));
#125599=CARTESIAN_POINT('',(16.0005576038968,39.1384565378295,-15.));
#125600=CARTESIAN_POINT('Origin',(16.0005576038968,36.1384565378295,-15.));
#125601=CARTESIAN_POINT('',(16.0005576038968,39.1384565378295,-12.));
#125602=CARTESIAN_POINT('Origin',(-16.0003574098591,36.1390276965147,-12.));
#125603=CARTESIAN_POINT('Origin',(-16.0003574098591,36.1390276965147,-15.));
#125604=CARTESIAN_POINT('Origin',(-15.8744846811456,36.139027695559,-15.));
#125605=CARTESIAN_POINT('Origin',(15.8746634037561,36.1384565378295,-15.));
#125606=CARTESIAN_POINT('',(16.5085576038968,35.6304565378295,-15.));
#125607=CARTESIAN_POINT('',(16.1916105038265,35.6304565378295,-15.));
#125608=CARTESIAN_POINT('',(16.0005576038968,36.1384565378295,-15.));
#125609=CARTESIAN_POINT('Origin',(16.5085576038968,36.1384565378295,-15.));
#125610=CARTESIAN_POINT('',(16.0005576038968,40.3844565378295,-15.));
#125611=CARTESIAN_POINT('Origin',(16.5085576038968,35.6304565378295,-26.));
#125612=CARTESIAN_POINT('',(16.5085576038968,35.6304565378295,-26.));
#125613=CARTESIAN_POINT('Origin',(16.5085576038968,36.1384565378295,-26.));
#125614=CARTESIAN_POINT('',(16.0005576038968,36.1384565378295,-26.));
#125615=CARTESIAN_POINT('Origin',(16.0005576038968,44.6304565378295,-26.));
#125616=CARTESIAN_POINT('',(16.0005576038968,44.6304565378295,-26.));
#125617=CARTESIAN_POINT('Origin',(15.5005576038968,44.6304565378295,-26.));
#215594=UNCERTAINTY_MEASURE_WITH_UNIT(LENGTH_MEASURE(0.01),#215610,
'DISTANCE_ACCURACY_VALUE',
'Maximum model space distance between geometric entities at asserted c
onnectivities');
#215598=UNCERTAINTY_MEASURE_WITH_UNIT(LENGTH_MEASURE(0.01),#215610,
'DISTANCE_ACCURACY_VALUE',
'Maximum model space distance between geometric entities at asserted c
onnectivities');
#215605=(
GEOMETRIC_REPRESENTATION_CONTEXT(3)
GLOBAL_UNCERTAINTY_ASSIGNED_CONTEXT((#215594))
GLOBAL_UNIT_ASSIGNED_CONTEXT((#215610,#215612,#215613))
REPRESENTATION_CONTEXT('','3D')
);
#215609=(
GEOMETRIC_REPRESENTATION_CONTEXT(3)
GLOBAL_UNCERTAINTY_ASSIGNED_CONTEXT((#215598))
GLOBAL_UNIT_ASSIGNED_CONTEXT((#215610,#215612,#215613))
REPRESENTATION_CONTEXT('','3D')
);
#215610=(
LENGTH_UNIT()
NAMED_UNIT(*)
SI_UNIT(.MILLI.,.METRE.)
);
#215612=(
NAMED_UNIT(*)
PLANE_ANGLE_UNIT()
SI_UNIT($,.RADIAN.)
);
#215613=(
NAMED_UNIT(*)
SI_UNIT($,.STERADIAN.)
SOLID_ANGLE_UNIT()
);
#215620=SHAPE_DEFINITION_REPRESENTATION(#215630,#215649);
#215630=PRODUCT_DEFINITION_SHAPE('',$,#215660);
#215649=SHAPE_REPRESENTATION('',(#28931),#215605);
#215653=PRODUCT_DEFINITION_CONTEXT('part definition',#215685,'design');
#215660=PRODUCT_DEFINITION('2026-10-04-16-01-39-984_1',
'CarregeSupport(Mirror)',#215670,#215653);
#215670=PRODUCT_DEFINITION_FORMATION('',$,#215693);
#215685=APPLICATION_CONTEXT(
'Core Data for Automotive Mechanical Design Process');
#215686=PRODUCT_CONTEXT('part definition',#215685,'mechanical');
#215693=PRODUCT('2026-10-04-16-01-39-984_1','CarregeSupport(Mirror)',$,
(#215686));
#215698=PRESENTATION_STYLE_ASSIGNMENT((#215700));
#215700=SURFACE_STYLE_USAGE(.BOTH.,#215702);
#215702=SURFACE_SIDE_STYLE('',(#215704));
#215704=SURFACE_STYLE_FILL_AREA(#215706);
#215706=FILL_AREA_STYLE('Opaque(245,245,246)',(#215708));
#215708=FILL_AREA_STYLE_COLOUR('Opaque(245,245,246)',#215710);
#215710=COLOUR_RGB('Opaque(245,245,246)', 0.66274510, 0.83137255, 0.94901961);
ENDSEC;
END-ISO-10303-21;
